ISO-10303-21;
HEADER;
FILE_DESCRIPTION (('STEP AP214'),
    '1' );
FILE_NAME ('hex flange bolt small_iso_ISO 4162 - M8 x 45 x 22-N.step',
    '2026-10-31T03:44:21',
    ( '' ),
    ( '' ),
    'SwSTEP 2.0',
    'SolidWorks 2026',
    '' );
FILE_SCHEMA (( 'AUTOMOTIVE_DESIGN' ));
ENDSEC;

DATA;
#12=CARTESIAN_POINT ( 'NONE',  ( 6.204460410672268722, -3.831267809382561840, 3.364049496746113199 ) ) ;
#79=EDGE_CURVE ( 'NONE', #3064, #8689, #14380, .T. ) ;
#91=CARTESIAN_POINT ( 'NONE',  ( 0.000000000000000000, -4.330127018922193649, -2.500000000000000000 ) ) ;
#109=CARTESIAN_POINT ( 'NONE',  ( 5.991014884144049368, -4.330127018922197202, -2.500000000000000444 ) ) ;
#112=CARTESIAN_POINT ( 'NONE',  ( 8.500000000000000000, 0.000000000000000000, 7.900000000000002132 ) ) ;
#120=CARTESIAN_POINT ( 'NONE',  ( 6.534533895392294234, 2.951347675328725106, 5.111884124469659341 ) ) ;
#133=CARTESIAN_POINT ( 'NONE',  ( 6.527192678185834929, 2.941622124011056272, -5.095038975456026797 ) ) ;
#167=EDGE_CURVE ( 'NONE', #12421, #12590, #7736, .T. ) ;
#247=CARTESIAN_POINT ( 'NONE',  ( 6.327625087026996553, 2.033113452595566972, -4.999999999998725464 ) ) ;
#267=CARTESIAN_POINT ( 'NONE',  ( 6.452281807715811723, -5.797857616945994330, 1.289641217033754180E-15 ) ) ;
#270=CONICAL_SURFACE ( 'NONE', #1210, 5.000000000000000000, 1.047197551196600296 ) ;
#340=EDGE_CURVE ( 'NONE', #6420, #12615, #2499, .T. ) ;
#374=B_SPLINE_CURVE_WITH_KNOTS ( 'NONE', 3,
 ( #17934, #13506, #10742, #16839, #1743, #16743 ),
 .UNSPECIFIED., .F., .F.,
 ( 4, 2, 4 ),
 ( 0.000000000000000000, 0.001488912493401906576, 0.002977824986803813152 ),
 .UNSPECIFIED. ) ;
#395=CARTESIAN_POINT ( 'NONE',  ( 6.371506350351443970, 3.439339428956429856, -4.260454149911179655 ) ) ;
#447=CONICAL_SURFACE ( 'NONE', #7021, 8.105212085995399107, 1.221730476396037490 ) ;
#459=CARTESIAN_POINT ( 'NONE',  ( 6.495567275915080430, -5.834887664329776236, 2.176274696337492837E-17 ) ) ;
#481=CARTESIAN_POINT ( 'NONE',  ( 6.534838248920899595, 5.903531555104835071, 8.098083288904839678E-18 ) ) ;
#486=CARTESIAN_POINT ( 'NONE',  ( 0.04201760816083378175, -0.9730571234388133428, 4.999999999999997335 ) ) ;
#490=PRODUCT_CONTEXT ( 'NONE', #11393, 'mechanical' ) ;
#504=EDGE_CURVE ( 'NONE', #8689, #19334, #374, .T. ) ;
#527=CARTESIAN_POINT ( 'NONE',  ( 6.390983399715594260, -5.837459000499769957, 0.1107755759658282380 ) ) ;
#588=CONICAL_SURFACE ( 'NONE', #5598, 5.000000000000000000, 1.047197551196600296 ) ;
#624=CARTESIAN_POINT ( 'NONE',  ( 6.541334219041339715, -5.921300567812618709, 0.03049376373817737351 ) ) ;
#638=CARTESIAN_POINT ( 'NONE',  ( 6.466260427357664042, -2.904280683598015500, -5.030361703432624232 ) ) ;
#651=EDGE_CURVE ( 'NONE', #13093, #10178, #4152, .T. ) ;
#655=CARTESIAN_POINT ( 'NONE',  ( 6.367873360227559232, -5.773502691896263528, 0.000000000000000000 ) ) ;
#656=CARTESIAN_POINT ( 'NONE',  ( 6.245824673232967861, -4.939548505213401164, 1.655093584844986143 ) ) ;
#691=B_SPLINE_CURVE_WITH_KNOTS ( 'NONE', 3,
 ( #18613, #5537, #5153, #3691, #8492, #11127, #2238, #17423, #17230, #15944, #18906, #8283, #8196, #11223, #14467, #18805 ),
 .UNSPECIFIED., .F., .F.,
 ( 4, 3, 3, 3, 3, 4 ),
 ( 0.000000000000000000, 5.303647860849932744E-05, 0.0001057093501027352823, 0.0001642058037231763413, 0.0002210073443958810151, 0.0002236769549542870245 ),
 .UNSPECIFIED. ) ;
#709=ORIENTED_EDGE ( 'NONE', *, *, #9739, .T. ) ;
#736=DIRECTION ( 'NONE',  ( -1.000000000000000000, 0.000000000000000000, -0.000000000000000000 ) ) ;
#751=DIRECTION ( 'NONE',  ( 0.000000000000000000, 0.000000000000000000, -1.000000000000000000 ) ) ;
#766=EDGE_CURVE ( 'NONE', #17828, #5258, #15091, .T. ) ;
#774=ORIENTED_EDGE ( 'NONE', *, *, #6694, .T. ) ;
#782=CARTESIAN_POINT ( 'NONE',  ( 6.271006797790669829, -0.9853839345309097775, -5.106080050406711202 ) ) ;
#822=CARTESIAN_POINT ( 'NONE',  ( 6.390983631292896483, 3.014665224428355383, 4.999999999999999112 ) ) ;
#834=CARTESIAN_POINT ( 'NONE',  ( 0.3108895250736384841, -2.416698868092693075, -5.000000000000000000 ) ) ;
#843=CIRCLE ( 'NONE', #5244, 4.000000000000000000 ) ;
#889=CARTESIAN_POINT ( 'NONE',  ( 7.336184427528458230, 0.000000000000000000, -8.105212085995399107 ) ) ;
#899=ORIENTED_EDGE ( 'NONE', *, *, #10276, .F. ) ;
#950=VERTEX_POINT ( 'NONE', #2906 ) ;
#984=CARTESIAN_POINT ( 'NONE',  ( 6.507056315241515954, 5.826803161468471437, -0.09231912136634902455 ) ) ;
#1003=ORIENTED_EDGE ( 'NONE', *, *, #7597, .F. ) ;
#1025=CARTESIAN_POINT ( 'NONE',  ( 6.390820551024316565, -3.013776919160863876, 4.999999999999999112 ) ) ;
#1032=CARTESIAN_POINT ( 'NONE',  ( 6.534838248920896930, -2.951765777552406878, 5.112608298763836601 ) ) ;
#1078=CARTESIAN_POINT ( 'NONE',  ( 6.506891779418573662, 2.833891091414751706, 5.091556646552823473 ) ) ;
#1088=B_SPLINE_CURVE_WITH_KNOTS ( 'NONE', 3,
 ( #13468, #9047, #4255, #4650, #4459 ),
 .UNSPECIFIED., .F., .F.,
 ( 4, 1, 4 ),
 ( 0.000000000000000000, 0.002886751345948131153, 0.005773502691896262307 ),
 .UNSPECIFIED. ) ;
#1090=CARTESIAN_POINT ( 'NONE',  ( 53.50000000000000000, 4.052968581778165278E-16, -3.309499999999999886 ) ) ;
#1164=AXIS2_PLACEMENT_3D ( 'NONE', #4910, #9218, #3632 ) ;
#1177=( BOUNDED_SURFACE ( )  B_SPLINE_SURFACE ( 3, 2, ( 
 ( #1025, #3764, #8259 ),
 ( #10023, #6987, #16024 ),
 ( #12680, #5618, #9629 ),
 ( #12967, #7084, #2610 ),
 ( #19077, #18681, #17108 ),
 ( #822, #15626, #6793 ) ),
 .UNSPECIFIED., .F., .F., .T. ) 
 B_SPLINE_SURFACE_WITH_KNOTS ( ( 4, 2, 4 ),
 ( 3, 3 ),
 ( 0.02367497856332483747, 0.02662799652435013376, 0.02958101448537543005 ),
 ( 0.000000000000000000, 1.000000000000000000 ),
 .UNSPECIFIED. ) 
 GEOMETRIC_REPRESENTATION_ITEM ( )  RATIONAL_B_SPLINE_SURFACE ( (
 ( 1.000000000000000000, 0.8047781226141854649, 1.000000000000000000),
 ( 1.000000000000000000, 0.8123782257049820821, 1.000000000000000000),
 ( 1.000000000000000000, 0.8190665358012705344, 1.000000000000000000),
 ( 1.000000000000000000, 0.8192358187342196896, 1.000000000000000000),
 ( 1.000000000000000000, 0.8126132506074239537, 1.000000000000000000),
 ( 1.000000000000000000, 0.8047712440299316095, 1.000000000000000000) ) ) 
 REPRESENTATION_ITEM ( '' )  SURFACE ( )  );
#1193=FACE_OUTER_BOUND ( 'NONE', #16326, .T. ) ;
#1200=CARTESIAN_POINT ( 'NONE',  ( 6.270568613849419215, -4.911887854652846386, -1.704496029161938875 ) ) ;
#1202=VERTEX_POINT ( 'NONE', #9438 ) ;
#1210=AXIS2_PLACEMENT_3D ( 'NONE', #7268, #4223, #10291 ) ;
#1221=AXIS2_PLACEMENT_3D ( 'NONE', #12128, #15173, #18237 ) ;
#1226=DIRECTION ( 'NONE',  ( 0.000000000000000000, -0.5000000000000011102, -0.8660254037844380415 ) ) ;
#1268=SURFACE_STYLE_FILL_AREA ( #16078 ) ;
#1271=B_SPLINE_CURVE_WITH_KNOTS ( 'NONE', 3,
 ( #7672, #13653, #4648, #7869, #133, #3464, #3364, #1704, #12462, #15320, #13842, #18473, #9045, #10608, #3088, #16902 ),
 .UNSPECIFIED., .F., .F.,
 ( 4, 3, 3, 3, 3, 4 ),
 ( -2.669610558406242719E-06, 0.000000000000000000, 5.703179328865551904E-05, 0.0001157653700805886653, 0.0001686517580799675017, 0.0002219032271235110720 ),
 .UNSPECIFIED. ) ;
#1318=( GEOMETRIC_REPRESENTATION_CONTEXT ( 3 ) GLOBAL_UNCERTAINTY_ASSIGNED_CONTEXT ( ( #16988 ) ) GLOBAL_UNIT_ASSIGNED_CONTEXT ( ( #19323, #10363, #12122 ) ) REPRESENTATION_CONTEXT ( 'NONE', 'WORKASPACE' ) );
#1332=DIRECTION ( 'NONE',  ( -1.000000000000000000, -0.000000000000000000, -0.000000000000000000 ) ) ;
#1337=VERTEX_POINT ( 'NONE', #17596 ) ;
#1356=CARTESIAN_POINT ( 'NONE',  ( 6.466260427357665819, 5.808561367196023895, -1.902591328531564046E-16 ) ) ;
#1363=( NAMED_UNIT ( * ) PLANE_ANGLE_UNIT ( ) SI_UNIT ( $, .RADIAN. ) );
#1389=ORIENTED_EDGE ( 'NONE', *, *, #18061, .F. ) ;
#1397=CARTESIAN_POINT ( 'NONE',  ( 0.000000000000000000, 0.000000000000000000, 5.000000000000000000 ) ) ;
#1406=CARTESIAN_POINT ( 'NONE',  ( 8.500000000000000000, 5.773502691896261751, 0.000000000000000000 ) ) ;
#1477=CARTESIAN_POINT ( 'NONE',  ( -3.917148844556152511E-15, -4.821944789745365334, 1.648146632869001094 ) ) ;
#1481=FACE_OUTER_BOUND ( 'NONE', #18132, .T. ) ;
#1491=CARTESIAN_POINT ( 'NONE',  ( 6.518095160331712989, 2.933089652807542524, 5.080260301817225432 ) ) ;
#1507=ORIENTED_EDGE ( 'NONE', *, *, #340, .F. ) ;
#1541=( GEOMETRIC_REPRESENTATION_CONTEXT ( 3 ) GLOBAL_UNCERTAINTY_ASSIGNED_CONTEXT ( ( #7542 ) ) GLOBAL_UNIT_ASSIGNED_CONTEXT ( ( #16270, #1363, #17843 ) ) REPRESENTATION_CONTEXT ( 'NONE', 'WORKASPACE' ) );
#1558=ORIENTED_EDGE ( 'NONE', *, *, #15871, .T. ) ;
#1605=DIRECTION ( 'NONE',  ( 0.000000000000000000, 0.000000000000000000, 1.000000000000000000 ) ) ;
#1624=DIRECTION ( 'NONE',  ( -1.000000000000000000, -0.000000000000000000, -0.000000000000000000 ) ) ;
#1627=CARTESIAN_POINT ( 'NONE',  ( 0.1996310553826630974, 1.947030205581109730, -5.000000000000000888 ) ) ;
#1641=CARTESIAN_POINT ( 'NONE',  ( 0.4465819873852039379, 5.773502691896261751, 3.331019006688249527E-17 ) ) ;
#1660=ORIENTED_EDGE ( 'NONE', *, *, #12863, .F. ) ;
#1666=CARTESIAN_POINT ( 'NONE',  ( 6.420058897733093239, 5.782965130189194447, -1.451745169709246731E-16 ) ) ;
#1689=CARTESIAN_POINT ( 'NONE',  ( 0.000000000000000000, 0.000000000000000000, 0.000000000000000000 ) ) ;
#1704=CARTESIAN_POINT ( 'NONE',  ( 6.495567275915088423, 2.917443832164887230, -5.053160945538039961 ) ) ;
#1719=CARTESIAN_POINT ( 'NONE',  ( 6.507056315241516842, -5.826803161468474102, 0.09231912136634916333 ) ) ;
#1743=CARTESIAN_POINT ( 'NONE',  ( 6.244297270355323448, 0.4917101305082447471, 5.105276777067912164 ) ) ;
#1749=ORIENTED_EDGE ( 'NONE', *, *, #12259, .T. ) ;
#1793=B_SPLINE_CURVE_WITH_KNOTS ( 'NONE', 3,
 ( #15572, #7735, #12336, #15380, #9389, #6174, #15188, #15284 ),
 .UNSPECIFIED., .F., .F.,
 ( 4, 2, 2, 4 ),
 ( 0.002921158011986723767, 0.003648658599403076588, 0.004376159186819428976, 0.005831160361652133750 ),
 .UNSPECIFIED. ) ;
#1808=LINE ( 'NONE', #7493, #11376 ) ;
#1814=AXIS2_PLACEMENT_3D ( 'NONE', #15108, #6091, #12061 ) ;
#1837=DIRECTION ( 'NONE',  ( 0.000000000000000000, 0.000000000000000000, 1.000000000000000000 ) ) ;
#1862=PRODUCT_DEFINITION_CONTEXT ( 'detailed design', #13036, 'design' ) ;
#1868=CARTESIAN_POINT ( 'NONE',  ( 6.244004651191001898, 4.178905357954649347, -2.972460101650454156 ) ) ;
#1903=AXIS2_PLACEMENT_3D ( 'NONE', #15026, #13166, #1605 ) ;
#1918=CARTESIAN_POINT ( 'NONE',  ( 6.212068001623061164, -3.310128279683368202, -4.266689640017852447 ) ) ;
#1923=FACE_OUTER_BOUND ( 'NONE', #13422, .T. ) ;
#1945=CARTESIAN_POINT ( 'NONE',  ( 8.500000000000000000, 5.773502691896261751, 0.000000000000000000 ) ) ;
#1952=DIRECTION ( 'NONE',  ( -1.000000000000000000, -0.000000000000000000, -0.000000000000000000 ) ) ;
#1953=ORIENTED_EDGE ( 'NONE', *, *, #18219, .T. ) ;
#1957=DIRECTION ( 'NONE',  ( 1.000000000000000000, 0.000000000000000000, -0.000000000000000000 ) ) ;
#1967=CARTESIAN_POINT ( 'NONE',  ( 0.1973348417602470706, -1.936114729415141733, 4.999999999999999112 ) ) ;
#1990=CARTESIAN_POINT ( 'NONE',  ( 6.244297270354683960, 1.802013835206515036E-11, 5.105276777067893512 ) ) ;
#1992=B_SPLINE_CURVE_WITH_KNOTS ( 'NONE', 3,
 ( #8740, #11767, #16305, #14716, #14817 ),
 .UNSPECIFIED., .F., .F.,
 ( 4, 1, 4 ),
 ( 0.000000000000000000, 0.002886751345948130286, 0.005773502691896260572 ),
 .UNSPECIFIED. ) ;
#2036=LINE ( 'NONE', #1945, #10351 ) ;
#2078=B_SPLINE_CURVE_WITH_KNOTS ( 'NONE', 3,
 ( #11055, #3614, #395, #12339, #1868, #6269, #9580, #481 ),
 .UNSPECIFIED., .F., .F.,
 ( 4, 2, 2, 4 ),
 ( 0.000000000000000000, 0.001493104274552340587, 0.002986208549104681607, 0.005972417098209364950 ),
 .UNSPECIFIED. ) ;
#2080=DIRECTION ( 'NONE',  ( 0.000000000000000000, 0.5000000000000009992, -0.8660254037844380415 ) ) ;
#2083=PLANE ( 'NONE',  #14222 ) ;
#2129=DIRECTION ( 'NONE',  ( -1.000000000000000000, -0.000000000000000000, -0.000000000000000000 ) ) ;
#2142=DIRECTION ( 'NONE',  ( 0.000000000000000000, 0.000000000000000000, 1.000000000000000000 ) ) ;
#2156=EDGE_CURVE ( 'NONE', #12421, #12768, #11090, .T. ) ;
#2163=CARTESIAN_POINT ( 'NONE',  ( 6.445379721942640749, -2.463581311471618740, -5.110653333236677476 ) ) ;
#2238=CARTESIAN_POINT ( 'NONE',  ( 6.466260427357672036, -2.904280683598005286, 5.030361703432631337 ) ) ;
#2239=DIRECTION ( 'NONE',  ( 0.000000000000000000, 0.000000000000000000, 1.000000000000000000 ) ) ;
#2332=CARTESIAN_POINT ( 'NONE',  ( 8.500000000000000000, -5.773502691896263528, 0.000000000000000000 ) ) ;
#2333=ORIENTED_EDGE ( 'NONE', *, *, #7597, .T. ) ;
#2334=ORIENTED_EDGE ( 'NONE', *, *, #17943, .F. ) ;
#2357=MANIFOLD_SOLID_BREP ( 'FlangeHexFillet', #11799 ) ;
#2361=EDGE_CURVE ( 'NONE', #10736, #18339, #18860, .T. ) ;
#2362=DIRECTION ( 'NONE',  ( 1.000000000000000000, 0.000000000000000000, -0.000000000000000000 ) ) ;
#2363=ADVANCED_FACE ( 'NONE', ( #3403 ), #4961, .T. ) ;
#2407=CARTESIAN_POINT ( 'NONE',  ( 8.500000000000000000, 5.773502691896261751, -2.749426538070115714E-16 ) ) ;
#2435=CARTESIAN_POINT ( 'NONE',  ( 0.4465819873849485311, -2.886751345948517677, -5.000000000000000000 ) ) ;
#2439=FACE_OUTER_BOUND ( 'NONE', #7094, .T. ) ;
#2443=ORIENTED_EDGE ( 'NONE', *, *, #2361, .T. ) ;
#2461=EDGE_CURVE ( 'NONE', #17113, #11939, #8509, .T. ) ;
#2482=DIRECTION ( 'NONE',  ( 0.000000000000000000, 0.000000000000000000, 1.000000000000000000 ) ) ;
#2499=B_SPLINE_CURVE_WITH_KNOTS ( 'NONE', 3,
 ( #5193, #4026, #15791, #14204 ),
 .UNSPECIFIED., .F., .F.,
 ( 4, 4 ),
 ( 0.002977824986803859555, 0.005972417098209359745 ),
 .UNSPECIFIED. ) ;
#2522=CARTESIAN_POINT ( 'NONE',  ( 0.000000000000000000, 0.000000000000000000, -5.000000000000000000 ) ) ;
#2523=VERTEX_POINT ( 'NONE', #11485 ) ;
#2529=CARTESIAN_POINT ( 'NONE',  ( 6.367873360227555679, -2.886751345948119774, 4.999999999999999112 ) ) ;
#2543=ORIENTED_EDGE ( 'NONE', *, *, #8682, .F. ) ;
#2572=EDGE_LOOP ( 'NONE', ( #4284, #18886, #10853, #13287, #10251 ) ) ;
#2588=CARTESIAN_POINT ( 'NONE',  ( 6.092449800118089343, 3.827241605637482724, -3.371023086194387286 ) ) ;
#2610=CARTESIAN_POINT ( 'NONE',  ( 6.242789945155967857, 0.9948955795114693412, 5.105232858000414708 ) ) ;
#2677=CARTESIAN_POINT ( 'NONE',  ( 0.4465819873851989974, -2.886751345948120218, 4.999999999999999112 ) ) ;
#2681=( BOUNDED_SURFACE ( )  B_SPLINE_SURFACE ( 3, 2, ( 
 ( #6327, #4572, #13950 ),
 ( #4768, #247, #6505 ),
 ( #7690, #12102, #12481 ),
 ( #9167, #15058, #3207 ),
 ( #13767, #7600, #4942 ),
 ( #3291, #4856, #15147 ) ),
 .UNSPECIFIED., .F., .F., .F. ) 
 B_SPLINE_SURFACE_WITH_KNOTS ( ( 4, 2, 4 ),
 ( 3, 3 ),
 ( 0.02368235114939812314, 0.02663560780161266378, 0.02958886445382720443 ),
 ( 0.000000000000000000, 1.000000000000000000 ),
 .UNSPECIFIED. ) 
 GEOMETRIC_REPRESENTATION_ITEM ( )  RATIONAL_B_SPLINE_SURFACE ( (
 ( 1.000000000000000000, 0.8047780980783513227, 1.000000000000000000),
 ( 1.000000000000000000, 0.8123789398383446381, 1.000000000000000000),
 ( 1.000000000000000000, 0.8190677725692530053, 1.000000000000000000),
 ( 1.000000000000000000, 0.8192346316605858547, 1.000000000000000000),
 ( 1.000000000000000000, 0.8126126875065289301, 1.000000000000000000),
 ( 1.000000000000000000, 0.8047712635281869531, 1.000000000000000000) ) ) 
 REPRESENTATION_ITEM ( '' )  SURFACE ( )  );
#2689=VERTEX_POINT ( 'NONE', #13645 ) ;
#2708=ORIENTED_EDGE ( 'NONE', *, *, #15391, .T. ) ;
#2720=ADVANCED_FACE ( 'NONE', ( #18181 ), #8520, .T. ) ;
#2752=( NAMED_UNIT ( * ) SI_UNIT ( $, .STERADIAN. ) SOLID_ANGLE_UNIT ( ) );
#2754=EDGE_LOOP ( 'NONE', ( #9771, #4011, #9063, #7040 ) ) ;
#2756=CARTESIAN_POINT ( 'NONE',  ( 6.357976367241986893, 5.421935536069748096, 0.8264656814052228073 ) ) ;
#2762=CARTESIAN_POINT ( 'NONE',  ( 0.05140428708382910328, -4.819072548984009607, -1.653121499799246719 ) ) ;
#2770=CARTESIAN_POINT ( 'NONE',  ( 0.01055556052338869899, -4.084588180558399451, 2.925285743277528105 ) ) ;
#2800=ORIENTED_EDGE ( 'NONE', *, *, #18948, .F. ) ;
#2819=VERTEX_POINT ( 'NONE', #14109 ) ;
#2840=CARTESIAN_POINT ( 'NONE',  ( 0.000000000000000000, 0.000000000000000000, 0.000000000000000000 ) ) ;
#2867=CARTESIAN_POINT ( 'NONE',  ( 0.000000000000000000, -4.330127018922188320, 2.500000000000010214 ) ) ;
#2871=CARTESIAN_POINT ( 'NONE',  ( 0.000000000000000000, 0.000000000000000000, 0.000000000000000000 ) ) ;
#2906=CARTESIAN_POINT ( 'NONE',  ( 0.000000000000000000, -4.330127018922188320, 2.500000000000010214 ) ) ;
#2970=CARTESIAN_POINT ( 'NONE',  ( 6.481779955677433591, 2.910222513313285742, 5.040653254389411586 ) ) ;
#3013=CARTESIAN_POINT ( 'NONE',  ( 0.000000000000000000, 0.000000000000000000, 0.000000000000000000 ) ) ;
#3033=CARTESIAN_POINT ( 'NONE',  ( -6.315157543962389260E-16, -3.838309248099061044, -3.351853367130940065 ) ) ;
#3064=VERTEX_POINT ( 'NONE', #18508 ) ;
#3072=CARTESIAN_POINT ( 'NONE',  ( 6.420058897733091463, 2.891482565094592339, 5.008194711943422028 ) ) ;
#3088=CARTESIAN_POINT ( 'NONE',  ( 6.385552186430389021, 2.886751345948122438, -5.000000000000001776 ) ) ;
#3100=CARTESIAN_POINT ( 'NONE',  ( 0.04320752586819883584, 0.9836842030436125928, -5.000000000000000000 ) ) ;
#3132=ORIENTED_EDGE ( 'NONE', *, *, #19173, .F. ) ;
#3153=CARTESIAN_POINT ( 'NONE',  ( 6.327632967270674591, -5.346704644969953790, 0.7392359018479527366 ) ) ;
#3169=CARTESIAN_POINT ( 'NONE',  ( 6.436591462021355348, 2.894509378375960118, 5.013437306331775645 ) ) ;
#3171=CARTESIAN_POINT ( 'NONE',  ( 6.367873360227556567, 2.886751345948125991, 4.999999999999999112 ) ) ;
#3182=ADVANCED_FACE ( 'NONE', ( #6908 ), #13275, .F. ) ;
#3202=CARTESIAN_POINT ( 'NONE',  ( 6.506891779418576327, -2.833891091414761032, -5.091556646552826138 ) ) ;
#3207=CARTESIAN_POINT ( 'NONE',  ( 6.242811304425483598, -0.9953138271174254426, -5.105233480330447549 ) ) ;
#3223=CARTESIAN_POINT ( 'NONE',  ( 5.991014884144048480, -4.770489558936219510E-15, -5.000000000000000000 ) ) ;
#3233=ORIENTED_EDGE ( 'NONE', *, *, #9384, .T. ) ;
#3238=CARTESIAN_POINT ( 'NONE',  ( 6.244004651191001010, -4.178905357954647570, 2.972460101650454600 ) ) ;
#3291=CARTESIAN_POINT ( 'NONE',  ( 6.390983168987730778, -3.014662706507984513, -5.000000000000000000 ) ) ;
#3301=EDGE_LOOP ( 'NONE', ( #9682, #10312, #5828, #1389, #4811 ) ) ;
#3324=CARTESIAN_POINT ( 'NONE',  ( 6.534838248920899595, 5.903531555104835071, 8.098083288904839678E-18 ) ) ;
#3334=CARTESIAN_POINT ( 'NONE',  ( 0.1996310553826632361, 1.947030205581113282, 4.999999999999997335 ) ) ;
#3350=EDGE_CURVE ( 'NONE', #3064, #12768, #1808, .T. ) ;
#3364=CARTESIAN_POINT ( 'NONE',  ( 6.506987859255528583, 2.925375531177297095, -5.066899051217877314 ) ) ;
#3371=FACE_OUTER_BOUND ( 'NONE', #18136, .T. ) ;
#3374=CARTESIAN_POINT ( 'NONE',  ( 0.3117969352650132309, 2.419842229202153305, -4.999999999999999112 ) ) ;
#3403=FACE_OUTER_BOUND ( 'NONE', #11668, .T. ) ;
#3406=CARTESIAN_POINT ( 'NONE',  ( 6.527192678185836705, -5.883244248022288403, -1.193258867985458992E-13 ) ) ;
#3428=ADVANCED_FACE ( 'NONE', ( #16330 ), #15133, .T. ) ;
#3464=CARTESIAN_POINT ( 'NONE',  ( 6.518095160331718319, 2.933089652807546077, -5.080260301817233426 ) ) ;
#3486=FACE_OUTER_BOUND ( 'NONE', #4110, .T. ) ;
#3504=CARTESIAN_POINT ( 'NONE',  ( 6.367873360227558344, -2.886751345948133984, -5.000000000000000000 ) ) ;
#3529=CARTESIAN_POINT ( 'NONE',  ( -4.997494388800372001E-16, -0.4883827417527024095, 4.999999999999999112 ) ) ;
#3585=CARTESIAN_POINT ( 'NONE',  ( 6.506987859255520590, -2.925375531177299759, -5.066899051217866656 ) ) ;
#3590=ADVANCED_FACE ( 'NONE', ( #3371 ), #447, .T. ) ;
#3597=CARTESIAN_POINT ( 'NONE',  ( 53.50000000000000000, 0.000000000000000000, 0.000000000000000000 ) ) ;
#3614=CARTESIAN_POINT ( 'NONE',  ( 6.445127866599365873, 3.194847394660948581, -4.687657648742338701 ) ) ;
#3632=DIRECTION ( 'NONE',  ( 0.000000000000000000, 0.000000000000000000, 1.000000000000000000 ) ) ;
#3658=DIRECTION ( 'NONE',  ( 0.000000000000000000, 0.000000000000000000, -1.000000000000000000 ) ) ;
#3674=ORIENTED_EDGE ( 'NONE', *, *, #2461, .T. ) ;
#3691=CARTESIAN_POINT ( 'NONE',  ( 6.420058897733096792, -2.891482565094587898, 5.008194711943423805 ) ) ;
#3699=EDGE_CURVE ( 'NONE', #12768, #12590, #15294, .T. ) ;
#3710=LINE ( 'NONE', #18922, #7728 ) ;
#3724=VECTOR ( 'NONE', #17343, 1000.000000000000000 ) ;
#3735=CARTESIAN_POINT ( 'NONE',  ( 6.355827204229362870, 3.436818823786758070, 4.264647808192652434 ) ) ;
#3745=DIRECTION ( 'NONE',  ( 0.000000000000000000, -0.5000000000000001110, 0.8660254037844387076 ) ) ;
#3762=EDGE_CURVE ( 'NONE', #17113, #3828, #4149, .T. ) ;
#3764=CARTESIAN_POINT ( 'NONE',  ( 6.506891485183659896, -2.992470280394939675, 5.000000000000000000 ) ) ;
#3770=AXIS2_PLACEMENT_3D ( 'NONE', #3013, #6233, #19412 ) ;
#3803=PLANE ( 'NONE',  #16893 ) ;
#3812=CARTESIAN_POINT ( 'NONE',  ( 0.000000000000000000, 4.330127018922190096, -2.500000000000006217 ) ) ;
#3817=EDGE_CURVE ( 'NONE', #5258, #3064, #8966, .T. ) ;
#3828=VERTEX_POINT ( 'NONE', #17776 ) ;
#3844=CARTESIAN_POINT ( 'NONE',  ( 6.323279575527231522, 3.325091652218045368, -4.240772318537636920 ) ) ;
#3854=CARTESIAN_POINT ( 'NONE',  ( 0.000000000000000000, 4.330127018922190985, 2.500000000000005329 ) ) ;
#3866=ORIENTED_EDGE ( 'NONE', *, *, #12259, .F. ) ;
#3894=DIRECTION ( 'NONE',  ( 1.000000000000000000, 0.000000000000000000, 0.000000000000000000 ) ) ;
#3917=EDGE_LOOP ( 'NONE', ( #10067, #2333, #5423 ) ) ;
#3924=CARTESIAN_POINT ( 'NONE',  ( 6.204460410672266946, 4.828986228461177532, 1.635950503255240607 ) ) ;
#3947=CARTESIAN_POINT ( 'NONE',  ( 6.367873360227559232, -5.773502691896263528, 0.000000000000000000 ) ) ;
#3960=DIRECTION ( 'NONE',  ( 1.000000000000000000, 0.000000000000000000, -0.000000000000000000 ) ) ;
#3983=AXIS2_PLACEMENT_3D ( 'NONE', #13808, #9110, #18049 ) ;
#3998=CARTESIAN_POINT ( 'NONE',  ( 0.05140428708382657752, 4.819072548984005167, 1.653121499799249605 ) ) ;
#4011=ORIENTED_EDGE ( 'NONE', *, *, #5676, .F. ) ;
#4012=CARTESIAN_POINT ( 'NONE',  ( 8.500000000000000000, -5.773502691896263528, 0.000000000000000000 ) ) ;
#4026=CARTESIAN_POINT ( 'NONE',  ( 6.244297270353404095, 0.9889575675955796230, -5.105276777067857097 ) ) ;
#4045=CARTESIAN_POINT ( 'NONE',  ( 6.534838248920899595, -2.951765777552420644, -5.112608298763837489 ) ) ;
#4049=CARTESIAN_POINT ( 'NONE',  ( 0.4465819873852002742, 2.886751345948125547, 4.999999999999999112 ) ) ;
#4059=FACE_OUTER_BOUND ( 'NONE', #13752, .T. ) ;
#4091=DIRECTION ( 'NONE',  ( -0.000000000000000000, 0.000000000000000000, -1.000000000000000000 ) ) ;
#4110=EDGE_LOOP ( 'NONE', ( #4990, #9146, #8929, #1507, #4681 ) ) ;
#4112=SURFACE_SIDE_STYLE ('',( #1268 ) ) ;
#4116=CARTESIAN_POINT ( 'NONE',  ( 6.323279575526388641, 5.335162385629701909, 0.7592276814629709270 ) ) ;
#4149=LINE ( 'NONE', #10113, #12965 ) ;
#4152=CIRCLE ( 'NONE', #9779, 0.5999999999999980904 ) ;
#4166=CARTESIAN_POINT ( 'NONE',  ( 0.4465819873849485311, -2.886751345948517677, -5.000000000000000000 ) ) ;
#4204=PRESENTATION_STYLE_ASSIGNMENT (( #5973 ) ) ;
#4205=CIRCLE ( 'NONE', #8886, 8.105212085995399107 ) ;
#4206=CARTESIAN_POINT ( 'NONE',  ( 6.534838248920897819, 2.951765777552411318, -5.112608298763837489 ) ) ;
#4209=CARTESIAN_POINT ( 'NONE',  ( 6.095473853218515536, 3.806361898857873793, 3.407187799183811983 ) ) ;
#4223=DIRECTION ( 'NONE',  ( 1.000000000000000000, 0.000000000000000000, 0.000000000000000000 ) ) ;
#4255=CARTESIAN_POINT ( 'NONE',  ( 5.991014884144048480, 4.330127018922193649, -2.499999999999998668 ) ) ;
#4260=EDGE_LOOP ( 'NONE', ( #4599, #14271, #8594 ) ) ;
#4284=ORIENTED_EDGE ( 'NONE', *, *, #6608, .F. ) ;
#4285=CARTESIAN_POINT ( 'NONE',  ( 0.4465819873852039379, 5.773502691896261751, 3.331019006688249527E-17 ) ) ;
#4335=CARTESIAN_POINT ( 'NONE',  ( 6.367873360227555679, -2.886751345948119774, 4.999999999999999112 ) ) ;
#4347=PLANE ( 'NONE',  #14691 ) ;
#4390=EDGE_CURVE ( 'NONE', #7769, #1337, #10793, .T. ) ;
#4419=CARTESIAN_POINT ( 'NONE',  ( 0.000000000000000000, -4.330127018922193649, -2.500000000000000000 ) ) ;
#4436=EDGE_CURVE ( 'NONE', #13007, #17145, #16274, .T. ) ;
#4449=DIRECTION ( 'NONE',  ( 0.000000000000000000, 0.000000000000000000, -1.000000000000000000 ) ) ;
#4451=B_SPLINE_CURVE_WITH_KNOTS ( 'NONE', 3,
 ( #13690, #6247, #11032, #14068, #3406, #16943, #6345, #459, #6432, #12411, #267, #10841, #12224, #18233, #12317, #655 ),
 .UNSPECIFIED., .F., .F.,
 ( 4, 3, 3, 3, 3, 4 ),
 ( -2.669610558405663348E-06, 0.000000000000000000, 5.703179328867284594E-05, 0.0001157653700806020010, 0.0001686517580799737359, 0.0002219032271235107196 ),
 .UNSPECIFIED. ) ;
#4459=CARTESIAN_POINT ( 'NONE',  ( 6.367873360227556567, 2.886751345948123770, -5.000000000000000000 ) ) ;
#4482=CARTESIAN_POINT ( 'NONE',  ( 53.50000000000000000, 0.000000000000000000, 0.000000000000000000 ) ) ;
#4486=ORIENTED_EDGE ( 'NONE', *, *, #13455, .T. ) ;
#4492=EDGE_CURVE ( 'NONE', #17668, #7530, #1793, .T. ) ;
#4509=ORIENTED_EDGE ( 'NONE', *, *, #17943, .T. ) ;
#4510=CARTESIAN_POINT ( 'NONE',  ( 6.495567275915080430, 5.834887664329775347, 9.410860448829699171E-16 ) ) ;
#4514=CARTESIAN_POINT ( 'NONE',  ( 6.355827204229362870, -5.411702751981846582, 0.8440485055075620524 ) ) ;
#4517=CARTESIAN_POINT ( 'NONE',  ( 0.4465819873852049926, -5.773502691896263528, -3.127607256515468906E-17 ) ) ;
#4525=CARTESIAN_POINT ( 'NONE',  ( 6.207530437345012864, -4.849805425595699937, 1.599890596045217439 ) ) ;
#4527=ORIENTED_EDGE ( 'NONE', *, *, #5708, .F. ) ;
#4536=CARTESIAN_POINT ( 'NONE',  ( 6.403457969954081008, 2.888443235695449030, 5.002930439003169028 ) ) ;
#4537=CARTESIAN_POINT ( 'NONE',  ( 6.196878017913830305, -1.924500897298744961, 4.999999999999999112 ) ) ;
#4572=CARTESIAN_POINT ( 'NONE',  ( 6.506892073925696351, 2.992473431090949543, -5.000000000000000000 ) ) ;
#4582=ORIENTED_EDGE ( 'NONE', *, *, #7956, .F. ) ;
#4599=ORIENTED_EDGE ( 'NONE', *, *, #11189, .T. ) ;
#4618=CARTESIAN_POINT ( 'NONE',  ( 6.541334219041335274, -2.934241909852036478, 5.143243597038029691 ) ) ;
#4621=ORIENTED_EDGE ( 'NONE', *, *, #651, .F. ) ;
#4622=CARTESIAN_POINT ( 'NONE',  ( 0.000000000000000000, -4.330127018922193649, -2.500000000000000000 ) ) ;
#4648=CARTESIAN_POINT ( 'NONE',  ( 6.534224484704323821, 2.950930484791612685, -5.111161529262899350 ) ) ;
#4650=CARTESIAN_POINT ( 'NONE',  ( 6.196878017913831194, 3.367876570272813730, -4.166666666666668739 ) ) ;
#4652=DIRECTION ( 'NONE',  ( -0.000000000000000000, 0.000000000000000000, 1.000000000000000000 ) ) ;
#4681=ORIENTED_EDGE ( 'NONE', *, *, #9384, .F. ) ;
#4768=CARTESIAN_POINT ( 'NONE',  ( 6.212060063025226064, 2.039954613758735658, -5.000000000000000000 ) ) ;
#4769=VERTEX_POINT ( 'NONE', #12921 ) ;
#4776=EDGE_LOOP ( 'NONE', ( #6330, #9142, #709, #16239 ) ) ;
#4785=B_SPLINE_CURVE_WITH_KNOTS ( 'NONE', 3,
 ( #17486, #19263, #17772, #1200, #19169, #7072, #10110, #4045 ),
 .UNSPECIFIED., .F., .F.,
 ( 4, 2, 2, 4 ),
 ( 1.228285202167177233E-19, 0.001493104274552340370, 0.002986208549104680306, 0.005972417098209360613 ),
 .UNSPECIFIED. ) ;
#4807=CARTESIAN_POINT ( 'NONE',  ( 0.000000000000000000, 0.000000000000000000, 5.000000000000000000 ) ) ;
#4811=ORIENTED_EDGE ( 'NONE', *, *, #18171, .F. ) ;
#4829=CARTESIAN_POINT ( 'NONE',  ( 0.4465819873852002742, 2.886751345948125547, 4.999999999999999112 ) ) ;
#4830=CARTESIAN_POINT ( 'NONE',  ( 53.50000000000000000, 0.000000000000000000, 3.309499999999999886 ) ) ;
#4856=CARTESIAN_POINT ( 'NONE',  ( 6.507056081706568129, -2.993351035583803110, -4.999999999999999112 ) ) ;
#4901=VERTEX_POINT ( 'NONE', #14576 ) ;
#4910=CARTESIAN_POINT ( 'NONE',  ( 0.000000000000000000, 0.000000000000000000, 0.000000000000000000 ) ) ;
#4915=CARTESIAN_POINT ( 'NONE',  ( 6.244889965166094292, 3.924082311521017274, 3.413878157001050795 ) ) ;
#4922=EDGE_LOOP ( 'NONE', ( #6440, #10323, #19281, #18216, #15107 ) ) ;
#4923=AXIS2_PLACEMENT_3D ( 'NONE', #6950, #2362, #17456 ) ;
#4929=DIRECTION ( 'NONE',  ( 0.000000000000000000, 0.000000000000000000, -1.000000000000000000 ) ) ;
#4930=CARTESIAN_POINT ( 'NONE',  ( 7.336184427528458230, 0.000000000000000000, 0.000000000000000000 ) ) ;
#4942=CARTESIAN_POINT ( 'NONE',  ( 6.357965579934049316, -1.995168835099641713, -5.108766517442258959 ) ) ;
#4951=CARTESIAN_POINT ( 'NONE',  ( 8.500000000000000000, 2.886751345948125991, 4.999999999999999112 ) ) ;
#4961=CYLINDRICAL_SURFACE ( 'NONE', #6322, 4.000000000000000000 ) ;
#4971=STYLED_ITEM ( 'NONE', ( #4204 ), #7556 ) ;
#4975=EDGE_CURVE ( 'NONE', #1337, #10178, #4205, .T. ) ;
#4990=ORIENTED_EDGE ( 'NONE', *, *, #11653, .T. ) ;
#5002=CARTESIAN_POINT ( 'NONE',  ( 52.80949999999998568, 0.000000000000000000, 4.000000000000000000 ) ) ;
#5062=CARTESIAN_POINT ( 'NONE',  ( 6.541171661047877173, -5.920857802016179505, -0.02973393389965061501 ) ) ;
#5103=CARTESIAN_POINT ( 'NONE',  ( 8.500000000000000000, 0.000000000000000000, 0.000000000000000000 ) ) ;
#5108=DIRECTION ( 'NONE',  ( -1.000000000000000000, -0.000000000000000000, -0.000000000000000000 ) ) ;
#5133=ORIENTED_EDGE ( 'NONE', *, *, #2461, .F. ) ;
#5142=FACE_OUTER_BOUND ( 'NONE', #4922, .T. ) ;
#5153=CARTESIAN_POINT ( 'NONE',  ( 6.403457969954084561, -2.888443235695444145, 5.002930439003169028 ) ) ;
#5154=CARTESIAN_POINT ( 'NONE',  ( 6.390820841722131718, -5.837016270311242039, -0.1100087447852515082 ) ) ;
#5187=CIRCLE ( 'NONE', #14254, 8.105212085995399107 ) ;
#5193=CARTESIAN_POINT ( 'NONE',  ( 6.244297270354684848, -1.798312406574552930E-11, -5.105276777067894400 ) ) ;
#5203=CARTESIAN_POINT ( 'NONE',  ( 6.390983399715591595, 2.822795037344616897, -5.110775575965828210 ) ) ;
#5244=AXIS2_PLACEMENT_3D ( 'NONE', #8249, #11578, #11478 ) ;
#5252=DIRECTION ( 'NONE',  ( 0.000000000000000000, 0.000000000000000000, 1.000000000000000000 ) ) ;
#5256=ORIENTED_EDGE ( 'NONE', *, *, #15871, .F. ) ;
#5258=VERTEX_POINT ( 'NONE', #7080 ) ;
#5288=CARTESIAN_POINT ( 'NONE',  ( 0.4465819873852049926, -5.773502691896263528, -3.127607256515468906E-17 ) ) ;
#5300=CARTESIAN_POINT ( 'NONE',  ( 6.362374563308228481, 5.433808049139812191, -0.8060918076009558897 ) ) ;
#5396=DIRECTION ( 'NONE',  ( 0.3420201433256622736, 0.000000000000000000, -0.9396926207859106484 ) ) ;
#5400=DIRECTION ( 'NONE',  ( 1.000000000000000000, 0.000000000000000000, 0.000000000000000000 ) ) ;
#5419=CARTESIAN_POINT ( 'NONE',  ( 53.50000000000000000, 4.475777889183788807E-16, -3.309499999999999886 ) ) ;
#5423=ORIENTED_EDGE ( 'NONE', *, *, #11783, .T. ) ;
#5477=CARTESIAN_POINT ( 'NONE',  ( 6.403457969954082785, 5.776886471390908717, -1.402224347649779865E-18 ) ) ;
#5496=CARTESIAN_POINT ( 'NONE',  ( 6.212068001623052282, 5.350125758160769962, -0.7333103599825900876 ) ) ;
#5507=CARTESIAN_POINT ( 'NONE',  ( 0.1739375980333722760, 3.358985280702821097, 4.182066831946702479 ) ) ;
#5516=ORIENTED_EDGE ( 'NONE', *, *, #18270, .T. ) ;
#5537=CARTESIAN_POINT ( 'NONE',  ( 6.385552186430388133, -2.886751345948118441, 5.000000000000000888 ) ) ;
#5538=CIRCLE ( 'NONE', #3983, 4.999999999999999112 ) ;
#5550=ORIENTED_EDGE ( 'NONE', *, *, #3699, .F. ) ;
#5555=CARTESIAN_POINT ( 'NONE',  ( 0.000000000000000000, 4.330127018922190985, 2.500000000000005329 ) ) ;
#5573=( NAMED_UNIT ( * ) PLANE_ANGLE_UNIT ( ) SI_UNIT ( $, .RADIAN. ) );
#5598=AXIS2_PLACEMENT_3D ( 'NONE', #9765, #3894, #751 ) ;
#5611=AXIS2_PLACEMENT_3D ( 'NONE', #10630, #13671, #18110 ) ;
#5618=CARTESIAN_POINT ( 'NONE',  ( 6.207541730803228575, -1.039448978216581665, 5.000000000000000888 ) ) ;
#5676=EDGE_CURVE ( 'NONE', #4769, #8689, #14417, .T. ) ;
#5682=EDGE_CURVE ( 'NONE', #5258, #2819, #15308, .T. ) ;
#5708=EDGE_CURVE ( 'NONE', #6420, #1337, #10185, .T. ) ;
#5725=CARTESIAN_POINT ( 'NONE',  ( 8.500000000000000000, 2.886751345948123770, -5.000000000000000000 ) ) ;
#5749=CARTESIAN_POINT ( 'NONE',  ( 0.000000000000000000, 4.330127018922190096, -2.500000000000006217 ) ) ;
#5791=CARTESIAN_POINT ( 'NONE',  ( -4.113721387458914807E-15, -4.207632145829740544, 2.712167343862823099 ) ) ;
#5799=EDGE_CURVE ( 'NONE', #18786, #11939, #14600, .T. ) ;
#5805=CARTESIAN_POINT ( 'NONE',  ( 6.533910050139694725, 2.950514251728050485, 5.110440592449069896 ) ) ;
#5828=ORIENTED_EDGE ( 'NONE', *, *, #5682, .T. ) ;
#5857=AXIS2_PLACEMENT_3D ( 'NONE', #11501, #17614, #14635 ) ;
#5862=CARTESIAN_POINT ( 'NONE',  ( 7.336184427528458230, 0.000000000000000000, 0.000000000000000000 ) ) ;
#5907=CARTESIAN_POINT ( 'NONE',  ( 0.000000000000000000, 0.000000000000000000, 0.000000000000000000 ) ) ;
#5918=EDGE_LOOP ( 'NONE', ( #15127, #17041, #7317 ) ) ;
#5973=SURFACE_STYLE_USAGE ( .BOTH. , #4112 ) ;
#5979=CARTESIAN_POINT ( 'NONE',  ( 6.534224484704327374, 5.901860969583204941, 2.029550679094937724E-14 ) ) ;
#6000=CARTESIAN_POINT ( 'NONE',  ( 6.390983399715589819, -2.822795037344614233, 5.110775575965824657 ) ) ;
#6049=FACE_OUTER_BOUND ( 'NONE', #17142, .T. ) ;
#6088=CARTESIAN_POINT ( 'NONE',  ( 6.367873360227559232, -5.773502691896263528, 0.000000000000000000 ) ) ;
#6091=DIRECTION ( 'NONE',  ( 1.000000000000000000, 0.000000000000000000, 0.000000000000000000 ) ) ;
#6157=EDGE_CURVE ( 'NONE', #12615, #4769, #2078, .T. ) ;
#6161=CARTESIAN_POINT ( 'NONE',  ( 6.506987859255521478, 5.850751062354592413, 1.196609732200561596E-15 ) ) ;
#6170=CARTESIAN_POINT ( 'NONE',  ( 6.270568613849412998, -3.932080789230354867, 3.401571648088637101 ) ) ;
#6174=CARTESIAN_POINT ( 'NONE',  ( 0.1983443223721567394, 3.359771601077105707, -4.180704885107416224 ) ) ;
#6204=CIRCLE ( 'NONE', #16544, 7.900000000000002132 ) ;
#6224=CARTESIAN_POINT ( 'NONE',  ( 6.245824673232814206, -3.903127342723638371, -3.450227696316022996 ) ) ;
#6233=DIRECTION ( 'NONE',  ( 1.000000000000000000, 0.000000000000000000, 0.000000000000000000 ) ) ;
#6247=CARTESIAN_POINT ( 'NONE',  ( 6.534533895392296010, -5.902695350657468865, 6.631005141235907328E-15 ) ) ;
#6269=CARTESIAN_POINT ( 'NONE',  ( 6.244889965166093404, 4.918546365148221078, -1.691415889817839302 ) ) ;
#6322=AXIS2_PLACEMENT_3D ( 'NONE', #16657, #15359, #13689 ) ;
#6327=CARTESIAN_POINT ( 'NONE',  ( 6.390821132688881967, 3.013780087859769363, -5.000000000000000000 ) ) ;
#6330=ORIENTED_EDGE ( 'NONE', *, *, #16111, .T. ) ;
#6345=CARTESIAN_POINT ( 'NONE',  ( 6.506987859255521478, -5.850751062354593302, 2.176274696337492837E-17 ) ) ;
#6366=CARTESIAN_POINT ( 'NONE',  ( 0.4465819873851989974, -2.886751345948120218, 4.999999999999999112 ) ) ;
#6386=EDGE_CURVE ( 'NONE', #12421, #950, #19150, .T. ) ;
#6403=AXIS2_PLACEMENT_3D ( 'NONE', #11658, #11955, #19241 ) ;
#6420=VERTEX_POINT ( 'NONE', #14680 ) ;
#6432=CARTESIAN_POINT ( 'NONE',  ( 6.481779955677436256, -5.820445026626584806, 1.740800559574606662E-15 ) ) ;
#6440=ORIENTED_EDGE ( 'NONE', *, *, #5682, .F. ) ;
#6505=CARTESIAN_POINT ( 'NONE',  ( 6.362366615495708366, 2.018765416950190961, -5.108861542006171597 ) ) ;
#6507=EDGE_CURVE ( 'NONE', #2689, #17828, #4451, .T. ) ;
#6563=CIRCLE ( 'NONE', #17547, 3.309499999999999886 ) ;
#6572=CARTESIAN_POINT ( 'NONE',  ( 6.270568613849413886, 4.911887854652841057, 1.704496029161937320 ) ) ;
#6590=EDGE_LOOP ( 'NONE', ( #9665, #5516, #4486, #13245, #9568 ) ) ;
#6608=EDGE_CURVE ( 'NONE', #9923, #13221, #2036, .T. ) ;
#6615=CARTESIAN_POINT ( 'NONE',  ( 6.452281807715810835, -2.898928808472999830, -5.021091983800332947 ) ) ;
#6629=CARTESIAN_POINT ( 'NONE',  ( 6.196878017913832970, -3.367876570272822168, -4.166666666666666963 ) ) ;
#6694=EDGE_CURVE ( 'NONE', #5258, #1202, #691, .T. ) ;
#6739=ADVANCED_FACE ( 'NONE', ( #12704 ), #11919, .T. ) ;
#6772=CARTESIAN_POINT ( 'NONE',  ( 6.506891779418572774, 5.826362946429627598, 0.09155664655281574305 ) ) ;
#6793=CARTESIAN_POINT ( 'NONE',  ( 6.541334450618642826, 2.987059910623326875, 5.112749838330405083 ) ) ;
#6853=DIRECTION ( 'NONE',  ( -1.000000000000000000, -0.000000000000000000, 0.000000000000000000 ) ) ;
#6865=CARTESIAN_POINT ( 'NONE',  ( 6.245824673233021151, 4.939548505212935758, -1.655093584846096366 ) ) ;
#6905=ORIENTED_EDGE ( 'NONE', *, *, #504, .F. ) ;
#6908=FACE_OUTER_BOUND ( 'NONE', #2572, .T. ) ;
#6950=CARTESIAN_POINT ( 'NONE',  ( 0.000000000000000000, 0.000000000000000000, 0.000000000000000000 ) ) ;
#6987=CARTESIAN_POINT ( 'NONE',  ( 6.327640840229819652, -2.033197012992983943, 4.999999999998298250 ) ) ;
#7021=AXIS2_PLACEMENT_3D ( 'NONE', #4930, #16909, #3658 ) ;
#7028=ORIENTED_EDGE ( 'NONE', *, *, #12633, .F. ) ;
#7040=ORIENTED_EDGE ( 'NONE', *, *, #12394, .F. ) ;
#7048=CARTESIAN_POINT ( 'NONE',  ( 6.541334219041338827, 5.921300567812616933, -0.03049376373817709943 ) ) ;
#7065=DIRECTION ( 'NONE',  ( -1.000000000000000000, -0.000000000000000000, -0.000000000000000000 ) ) ;
#7072=CARTESIAN_POINT ( 'NONE',  ( 6.244889965166096069, -3.924082311521025712, -3.413878157001049907 ) ) ;
#7078=B_SPLINE_CURVE_WITH_KNOTS ( 'NONE', 3,
 ( #8126, #2163, #16879, #782, #14102, #9588 ),
 .UNSPECIFIED., .F., .F.,
 ( 4, 2, 4 ),
 ( 4.336808689942017736E-19, 0.001488912493401929995, 0.002977824986803859555 ),
 .UNSPECIFIED. ) ;
#7080=CARTESIAN_POINT ( 'NONE',  ( 6.367873360227555679, -2.886751345948119774, 4.999999999999999112 ) ) ;
#7084=CARTESIAN_POINT ( 'NONE',  ( 6.204449577088272605, 0.9975080636026212311, 5.000000000000000000 ) ) ;
#7085=EDGE_LOOP ( 'NONE', ( #2543, #2443, #11047, #8419, #10414 ) ) ;
#7094=EDGE_LOOP ( 'NONE', ( #4582, #1003, #13263, #10631, #13791, #7028 ) ) ;
#7120=B_SPLINE_CURVE_WITH_KNOTS ( 'NONE', 3,
 ( #2522, #12979, #13179, #19089, #834, #4166 ),
 .UNSPECIFIED., .F., .F.,
 ( 4, 2, 4 ),
 ( 0.01799235506992015107, 0.01945319861728521740, 0.02091404216465028373 ),
 .UNSPECIFIED. ) ;
#7125=CARTESIAN_POINT ( 'NONE',  ( 7.336184427528458230, 9.926022037524705097E-16, 8.105212085995399107 ) ) ;
#7167=TOROIDAL_SURFACE ( 'NONE', #1221, 7.900000000000002132, 0.5999999999999979794 ) ;
#7217=CARTESIAN_POINT ( 'NONE',  ( 0.1739375980333736638, 5.301268757141562205, -0.8179331680533008520 ) ) ;
#7225=AXIS2_PLACEMENT_3D ( 'NONE', #18707, #9845, #5252 ) ;
#7226=CARTESIAN_POINT ( 'NONE',  ( -3.114822491369819039E-15, 4.452621892014636096, 2.287832656137190668 ) ) ;
#7236=CIRCLE ( 'NONE', #18218, 4.999999999999999112 ) ;
#7268=CARTESIAN_POINT ( 'NONE',  ( 0.000000000000000000, 0.000000000000000000, 0.000000000000000000 ) ) ;
#7317=ORIENTED_EDGE ( 'NONE', *, *, #4436, .T. ) ;
#7401=LINE ( 'NONE', #8485, #7757 ) ;
#7407=ORIENTED_EDGE ( 'NONE', *, *, #18061, .T. ) ;
#7432=ORIENTED_EDGE ( 'NONE', *, *, #7956, .T. ) ;
#7455=CARTESIAN_POINT ( 'NONE',  ( 0.000000000000000000, -4.330127018922188320, 2.500000000000010214 ) ) ;
#7463=VECTOR ( 'NONE', #15974, 1000.000000000000000 ) ;
#7467=CARTESIAN_POINT ( 'NONE',  ( 6.534224484704324709, 2.950930484791589148, 5.111161529262913561 ) ) ;
#7493=CARTESIAN_POINT ( 'NONE',  ( 8.500000000000000000, 2.886751345948125991, 4.999999999999999112 ) ) ;
#7507=ORIENTED_EDGE ( 'NONE', *, *, #12863, .T. ) ;
#7530=VERTEX_POINT ( 'NONE', #18582 ) ;
#7531=CARTESIAN_POINT ( 'NONE',  ( 0.4465819873849485311, -2.886751345948517677, -5.000000000000000000 ) ) ;
#7542=UNCERTAINTY_MEASURE_WITH_UNIT (LENGTH_MEASURE( 1.000000000000000082E-05 ), #16270, 'distance_accuracy_value', 'NONE');
#7556=ADVANCED_BREP_SHAPE_REPRESENTATION ( '', ( #2357, #10359 ), #1541 ) ;
#7573=FACE_OUTER_BOUND ( 'NONE', #14480, .T. ) ;
#7597=EDGE_CURVE ( 'NONE', #13007, #2523, #18689, .T. ) ;
#7600=CARTESIAN_POINT ( 'NONE',  ( 6.323268674613562013, -2.010012106699304191, -5.000000000001305622 ) ) ;
#7633=ORIENTED_EDGE ( 'NONE', *, *, #11189, .F. ) ;
#7672=CARTESIAN_POINT ( 'NONE',  ( 6.534838248920897819, 2.951765777552411318, -5.112608298763837489 ) ) ;
#7676=CARTESIAN_POINT ( 'NONE',  ( 52.80949999999998568, 4.898587196589412829E-16, -4.000000000000000000 ) ) ;
#7687=CARTESIAN_POINT ( 'NONE',  ( 6.323279575528418128, -5.335162385627848280, -0.7592276814619393077 ) ) ;
#7690=CARTESIAN_POINT ( 'NONE',  ( 6.095462721915160920, 1.047438013718291705, -5.000000000000000000 ) ) ;
#7691=ORIENTED_EDGE ( 'NONE', *, *, #9992, .F. ) ;
#7728=VECTOR ( 'NONE', #15672, 1000.000000000000000 ) ;
#7735=CARTESIAN_POINT ( 'NONE',  ( -3.417495597855351487E-15, 4.207632145829744097, -2.712167343862822655 ) ) ;
#7736=CIRCLE ( 'NONE', #1164, 5.000000000000000000 ) ;
#7742=CARTESIAN_POINT ( 'NONE',  ( 6.092449800118089343, -3.827241605636891641, 3.371023086195408247 ) ) ;
#7757=VECTOR ( 'NONE', #1332, 1000.000000000000000 ) ;
#7769=VERTEX_POINT ( 'NONE', #8820 ) ;
#7785=CARTESIAN_POINT ( 'NONE',  ( 6.362374563308273778, -3.415000007734520171, -4.302769906043296011 ) ) ;
#7797=CARTESIAN_POINT ( 'NONE',  ( 6.518095160331714766, -2.933089652807550074, -5.080260301817226321 ) ) ;
#7842=ORIENTED_EDGE ( 'NONE', *, *, #11653, .F. ) ;
#7869=CARTESIAN_POINT ( 'NONE',  ( 6.533910050139693837, 2.950514251728067361, -5.110440592449059238 ) ) ;
#7885=CARTESIAN_POINT ( 'NONE',  ( 6.207530437345013752, -3.810448612250145750, -3.400109403952246367 ) ) ;
#7952=DIRECTION ( 'NONE',  ( -0.7071067811865530128, 0.000000000000000000, 0.7071067811865421326 ) ) ;
#7956=EDGE_CURVE ( 'NONE', #2523, #17668, #5538, .T. ) ;
#7997=EDGE_CURVE ( 'NONE', #18339, #13933, #3710, .T. ) ;
#7998=ORIENTED_EDGE ( 'NONE', *, *, #10276, .T. ) ;
#8013=B_SPLINE_CURVE_WITH_KNOTS ( 'NONE', 3,
 ( #15046, #3374, #1627, #3100, #13375, #13758 ),
 .UNSPECIFIED., .F., .F.,
 ( 4, 2, 4 ),
 ( 0.01506847346324404271, 0.01653041426658209689, 0.01799235506992015107 ),
 .UNSPECIFIED. ) ;
#8053=DIRECTION ( 'NONE',  ( 1.000000000000000000, 0.000000000000000000, -0.000000000000000000 ) ) ;
#8080=CARTESIAN_POINT ( 'NONE',  ( 6.533910050139696502, -2.950514251728084236, -5.110440592449055686 ) ) ;
#8087=MECHANICAL_DESIGN_GEOMETRIC_PRESENTATION_REPRESENTATION('',(#4971),#12476);
#8094=ORIENTED_EDGE ( 'NONE', *, *, #13270, .T. ) ;
#8126=CARTESIAN_POINT ( 'NONE',  ( 6.534838248920899595, -2.951765777552420644, -5.112608298763837489 ) ) ;
#8145=FACE_OUTER_BOUND ( 'NONE', #4776, .T. ) ;
#8180=CARTESIAN_POINT ( 'NONE',  ( 6.436591462021357124, -2.894509378375969000, -5.013437306331776533 ) ) ;
#8189=DIRECTION ( 'NONE',  ( 0.000000000000000000, 0.000000000000000000, -1.000000000000000000 ) ) ;
#8196=CARTESIAN_POINT ( 'NONE',  ( 6.533910050139693837, -2.950514251728023840, 5.110440592449081443 ) ) ;
#8197=CARTESIAN_POINT ( 'NONE',  ( 6.196878017913834746, -5.292377467571577121, -0.8333333333333331483 ) ) ;
#8211=LINE ( 'NONE', #12820, #18529 ) ;
#8243=CARTESIAN_POINT ( 'NONE',  ( 8.500000000000000000, -2.886751345948133984, -5.000000000000000000 ) ) ;
#8249=CARTESIAN_POINT ( 'NONE',  ( 52.80949999999998568, 0.000000000000000000, 0.000000000000000000 ) ) ;
#8259=CARTESIAN_POINT ( 'NONE',  ( 6.541171370350062020, -2.986177670315871335, 5.112746295475706582 ) ) ;
#8283=CARTESIAN_POINT ( 'NONE',  ( 6.527192678185834929, -2.941622124011297412, 5.095038975455882913 ) ) ;
#8284=DIRECTION ( 'NONE',  ( 0.000000000000000000, 0.5000000000000018874, 0.8660254037844375974 ) ) ;
#8335=CARTESIAN_POINT ( 'NONE',  ( 6.541171661047875396, 5.920857802016174176, 0.02973393389964464062 ) ) ;
#8358=CARTESIAN_POINT ( 'NONE',  ( 8.500000000000000000, 4.898587196589412829E-16, -4.000000000000000000 ) ) ;
#8391=DIRECTION ( 'NONE',  ( 1.000000000000000000, 0.000000000000000000, -0.000000000000000000 ) ) ;
#8419=ORIENTED_EDGE ( 'NONE', *, *, #11783, .F. ) ;
#8439=CARTESIAN_POINT ( 'NONE',  ( 6.204460410672268722, 3.831267809383005041, -3.364049496745006529 ) ) ;
#8456=AXIS2_PLACEMENT_3D ( 'NONE', #2332, #13091, #8284 ) ;
#8470=CARTESIAN_POINT ( 'NONE',  ( 6.244297270354683960, 1.802013835206515036E-11, 5.105276777067893512 ) ) ;
#8485=CARTESIAN_POINT ( 'NONE',  ( 8.500000000000000000, 2.886751345948123770, -5.000000000000000000 ) ) ;
#8492=CARTESIAN_POINT ( 'NONE',  ( 6.436591462021362453, -2.894509378375957009, 5.013437306331779197 ) ) ;
#8509=CIRCLE ( 'NONE', #10386, 4.000000000000000000 ) ;
#8520=CONICAL_SURFACE ( 'NONE', #16987, 5.000000000000000000, 1.047197551196600296 ) ;
#8526=CARTESIAN_POINT ( 'NONE',  ( 6.390820841722129941, 2.823237767533145703, 5.110008744785254464 ) ) ;
#8545=B_SPLINE_CURVE_WITH_KNOTS ( 'NONE', 3,
 ( #5555, #7226, #14569, #3998, #11529, #19017, #17537, #4285 ),
 .UNSPECIFIED., .F., .F.,
 ( 4, 2, 2, 4 ),
 ( 0.002921158011986707288, 0.003648658599403064012, 0.004376159186819420302, 0.005831160361652131148 ),
 .UNSPECIFIED. ) ;
#8580=CARTESIAN_POINT ( 'NONE',  ( 6.534838248920897819, 2.951765777552412651, 5.112608298763836601 ) ) ;
#8594=ORIENTED_EDGE ( 'NONE', *, *, #12633, .T. ) ;
#8682=EDGE_CURVE ( 'NONE', #10736, #7530, #7401, .T. ) ;
#8689=VERTEX_POINT ( 'NONE', #8580 ) ;
#8708=SHAPE_REPRESENTATION_RELATIONSHIP ( 'NONE' , 'NONE' ,  #13428, #7556 ) ;
#8712=CARTESIAN_POINT ( 'NONE',  ( 6.390983399715593372, 5.837459000499768180, -0.1107755759658281131 ) ) ;
#8728=CARTESIAN_POINT ( 'NONE',  ( 0.08165819712376803929, -3.720292241887084295, 3.556264818047238041 ) ) ;
#8740=CARTESIAN_POINT ( 'NONE',  ( 6.367873360227556567, 2.886751345948125991, 4.999999999999999112 ) ) ;
#8778=CONICAL_SURFACE ( 'NONE', #1903, 3.309499999999999886, 0.7853981633974407295 ) ;
#8782=EDGE_CURVE ( 'NONE', #7530, #2523, #8013, .T. ) ;
#8787=PRODUCT_DEFINITION ( 'UNKNOWN', '', #12608, #1862 ) ;
#8807=ORIENTED_EDGE ( 'NONE', *, *, #4975, .F. ) ;
#8820=CARTESIAN_POINT ( 'NONE',  ( 8.500000000000000000, 9.800365875394399578E-16, -7.900000000000002132 ) ) ;
#8834=DIRECTION ( 'NONE',  ( 0.000000000000000000, 0.000000000000000000, 1.000000000000000000 ) ) ;
#8852=PLANE ( 'NONE',  #13175 ) ;
#8886=AXIS2_PLACEMENT_3D ( 'NONE', #5862, #11830, #17833 ) ;
#8900=( LENGTH_UNIT ( ) NAMED_UNIT ( * ) SI_UNIT ( .MILLI., .METRE. ) );
#8904=CARTESIAN_POINT ( 'NONE',  ( 6.518095160331716542, 5.866179305615093043, 1.445124054326800857E-15 ) ) ;
#8915=EDGE_CURVE ( 'NONE', #13221, #17668, #15280, .T. ) ;
#8922=CARTESIAN_POINT ( 'NONE',  ( 0.4465819873852049926, -5.773502691896263528, -3.127607256515468906E-17 ) ) ;
#8929=ORIENTED_EDGE ( 'NONE', *, *, #16111, .F. ) ;
#8966=B_SPLINE_CURVE_WITH_KNOTS ( 'NONE', 3,
 ( #4335, #4537, #10595, #16597, #3171 ),
 .UNSPECIFIED., .F., .F.,
 ( 4, 1, 4 ),
 ( 0.000000000000000000, 0.002886751345948122913, 0.005773502691896245827 ),
 .UNSPECIFIED. ) ;
#9005=CARTESIAN_POINT ( 'NONE',  ( 6.534838248920900483, -5.903531555104836848, 4.671345613696493211E-16 ) ) ;
#9009=CARTESIAN_POINT ( 'NONE',  ( -7.092489211676000613E-16, -4.452621892014641425, -2.287832656137186671 ) ) ;
#9018=ORIENTED_EDGE ( 'NONE', *, *, #6507, .F. ) ;
#9038=ADVANCED_FACE ( 'NONE', ( #11178 ), #2083, .F. ) ;
#9045=CARTESIAN_POINT ( 'NONE',  ( 6.420058897733097680, 2.891482565094591006, -5.008194711943424693 ) ) ;
#9047=CARTESIAN_POINT ( 'NONE',  ( 6.196878017913830305, 5.292377467571572680, -0.8333333333333333703 ) ) ;
#9050=PLANE ( 'NONE',  #16644 ) ;
#9063=ORIENTED_EDGE ( 'NONE', *, *, #9739, .F. ) ;
#9083=VECTOR ( 'NONE', #17375, 999.9999999999998863 ) ;
#9102=ORIENTED_EDGE ( 'NONE', *, *, #504, .T. ) ;
#9110=DIRECTION ( 'NONE',  ( 1.000000000000000000, 0.000000000000000000, -0.000000000000000000 ) ) ;
#9119=CARTESIAN_POINT ( 'NONE',  ( 6.095473853218515536, -4.853892138987517590, 1.592812200814445633 ) ) ;
#9140=DIRECTION ( 'NONE',  ( 0.000000000000000000, -0.8660254037844380415, -0.5000000000000009992 ) ) ;
#9142=ORIENTED_EDGE ( 'NONE', *, *, #10943, .F. ) ;
#9146=ORIENTED_EDGE ( 'NONE', *, *, #2361, .F. ) ;
#9164=CARTESIAN_POINT ( 'NONE',  ( 6.541171661047877173, -2.934678558896545386, -5.142480235691130552 ) ) ;
#9167=CARTESIAN_POINT ( 'NONE',  ( 6.092460485788117275, -1.005982284679170391, -5.000000000000000000 ) ) ;
#9187=VERTEX_POINT ( 'NONE', #19258 ) ;
#9193=CARTESIAN_POINT ( 'NONE',  ( 6.527192678185836705, 5.883244248022287515, -9.347031149521713219E-14 ) ) ;
#9196=ORIENTED_EDGE ( 'NONE', *, *, #4390, .T. ) ;
#9198=CARTESIAN_POINT ( 'NONE',  ( 6.244889965166096957, -4.918546365148221078, 1.691415889817839746 ) ) ;
#9218=DIRECTION ( 'NONE',  ( -1.000000000000000000, -0.000000000000000000, -0.000000000000000000 ) ) ;
#9238=CARTESIAN_POINT ( 'NONE',  ( 0.000000000000000000, 0.000000000000000000, 0.000000000000000000 ) ) ;
#9270=CARTESIAN_POINT ( 'NONE',  ( 6.196878017913830305, 1.924500897298746960, -4.999999999999999112 ) ) ;
#9288=EDGE_LOOP ( 'NONE', ( #7998, #19277, #5133, #3132 ) ) ;
#9296=CARTESIAN_POINT ( 'NONE',  ( 0.3117969352650131198, 2.419842229202155970, 4.999999999999999112 ) ) ;
#9384=EDGE_CURVE ( 'NONE', #9187, #6420, #7078, .T. ) ;
#9389=CARTESIAN_POINT ( 'NONE',  ( 0.08165819712376902462, 3.720292241887087403, -3.556264818047239817 ) ) ;
#9400=CARTESIAN_POINT ( 'NONE',  ( 0.3108895250735811966, -2.416698868092462149, 4.999999999999999112 ) ) ;
#9409=( BOUNDED_SURFACE ( )  B_SPLINE_SURFACE ( 3, 2, ( 
 ( #18754, #6772, #8335 ),
 ( #5496, #15800, #5300 ),
 ( #12658, #18859, #6865 ),
 ( #2588, #8439, #17283 ),
 ( #11466, #3844, #11174 ),
 ( #5203, #9706, #9804 ) ),
 .UNSPECIFIED., .F., .F., .F. ) 
 B_SPLINE_SURFACE_WITH_KNOTS ( ( 4, 2, 4 ),
 ( 3, 3 ),
 ( 0.02367865728600889938, 0.02663179453327095547, 0.02958493178053301503 ),
 ( 0.000000000000000000, 1.000000000000000000 ),
 .UNSPECIFIED. ) 
 GEOMETRIC_REPRESENTATION_ITEM ( )  RATIONAL_B_SPLINE_SURFACE ( (
 ( 1.000000000000000000, 0.8047781103519390244, 1.000000000000000000),
 ( 1.000000000000000000, 0.8123785825980075481, 1.000000000000000000),
 ( 1.000000000000000000, 0.8190671539288042480, 1.000000000000000000),
 ( 1.000000000000000000, 0.8192352255335092481, 1.000000000000000000),
 ( 1.000000000000000000, 0.8126129676835915916, 1.000000000000000000),
 ( 1.000000000000000000, 0.8047712537969718971, 1.000000000000000000) ) ) 
 REPRESENTATION_ITEM ( '' )  SURFACE ( )  );
#9438=CARTESIAN_POINT ( 'NONE',  ( 6.534838248920896930, -2.951765777552406878, 5.112608298763836601 ) ) ;
#9446=CARTESIAN_POINT ( 'NONE',  ( 6.390820841722131718, -2.823237767533154141, -5.110008744785255352 ) ) ;
#9453=B_SPLINE_CURVE_WITH_KNOTS ( 'NONE', 3,
 ( #2867, #5791, #2770, #10188, #8728, #11666, #16094, #2677 ),
 .UNSPECIFIED., .F., .F.,
 ( 4, 2, 2, 4 ),
 ( 0.002921158011986727237, 0.003648658599403079624, 0.004376159186819432445, 0.005831160361652135485 ),
 .UNSPECIFIED. ) ;
#9535=CARTESIAN_POINT ( 'NONE',  ( 6.357976367241527704, -5.421935536068480666, -0.8264656814046078548 ) ) ;
#9537=ORIENTED_EDGE ( 'NONE', *, *, #11095, .T. ) ;
#9568=ORIENTED_EDGE ( 'NONE', *, *, #13480, .F. ) ;
#9580=CARTESIAN_POINT ( 'NONE',  ( 6.355827204229362870, 5.411702751981843917, -0.8440485055075606091 ) ) ;
#9588=CARTESIAN_POINT ( 'NONE',  ( 6.244297270354684848, -1.798312406574552930E-11, -5.105276777067894400 ) ) ;
#9629=CARTESIAN_POINT ( 'NONE',  ( 6.245835795331710294, -1.036512332922514767, 5.105321605219339531 ) ) ;
#9644=CARTESIAN_POINT ( 'NONE',  ( 6.420058897733093239, -2.891482565094600776, -5.008194711943422917 ) ) ;
#9665=ORIENTED_EDGE ( 'NONE', *, *, #7997, .F. ) ;
#9666=CARTESIAN_POINT ( 'NONE',  ( 6.367873360227558344, 5.773502691896261751, 0.000000000000000000 ) ) ;
#9682=ORIENTED_EDGE ( 'NONE', *, *, #13455, .F. ) ;
#9697=CONICAL_SURFACE ( 'NONE', #18189, 5.000000000000000000, 1.047197551196600296 ) ;
#9706=CARTESIAN_POINT ( 'NONE',  ( 6.507056315241514177, 2.833450876375910976, -5.092319121366348789 ) ) ;
#9737=ADVANCED_FACE ( 'NONE', ( #9980 ), #16074, .F. ) ;
#9739=EDGE_CURVE ( 'NONE', #9923, #4769, #12066, .T. ) ;
#9765=CARTESIAN_POINT ( 'NONE',  ( 0.000000000000000000, 0.000000000000000000, 0.000000000000000000 ) ) ;
#9771=ORIENTED_EDGE ( 'NONE', *, *, #79, .T. ) ;
#9779=AXIS2_PLACEMENT_3D ( 'NONE', #18510, #14062, #8189 ) ;
#9804=CARTESIAN_POINT ( 'NONE',  ( 6.541334219041337050, 2.934241909852039143, -5.143243597038033244 ) ) ;
#9825=ORIENTED_EDGE ( 'NONE', *, *, #766, .F. ) ;
#9845=DIRECTION ( 'NONE',  ( -1.000000000000000000, -0.000000000000000000, -0.000000000000000000 ) ) ;
#9846=FACE_OUTER_BOUND ( 'NONE', #3301, .T. ) ;
#9923=VERTEX_POINT ( 'NONE', #9666 ) ;
#9980=FACE_OUTER_BOUND ( 'NONE', #2754, .T. ) ;
#9992=EDGE_CURVE ( 'NONE', #10178, #1337, #5187, .T. ) ;
#10023=CARTESIAN_POINT ( 'NONE',  ( 6.212075932873402984, -2.040040303548923628, 4.999999999999999112 ) ) ;
#10027=ORIENTED_EDGE ( 'NONE', *, *, #6507, .T. ) ;
#10035=ORIENTED_EDGE ( 'NONE', *, *, #11095, .F. ) ;
#10067=ORIENTED_EDGE ( 'NONE', *, *, #13480, .T. ) ;
#10110=CARTESIAN_POINT ( 'NONE',  ( 6.355827204229362870, -3.436818823786764288, -4.264647808192651546 ) ) ;
#10113=CARTESIAN_POINT ( 'NONE',  ( 0.000000000000000000, 0.000000000000000000, 4.000000000000000000 ) ) ;
#10121=CARTESIAN_POINT ( 'NONE',  ( 8.500000000000000000, 0.000000000000000000, 0.000000000000000000 ) ) ;
#10124=FACE_OUTER_BOUND ( 'NONE', #7085, .T. ) ;
#10176=CARTESIAN_POINT ( 'NONE',  ( 6.207530437345011087, 3.810448612249821565, 3.400109403952575882 ) ) ;
#10178=VERTEX_POINT ( 'NONE', #7125 ) ;
#10185=LINE ( 'NONE', #889, #14760 ) ;
#10188=CARTESIAN_POINT ( 'NONE',  ( 0.05140428708382505096, -3.841181488860373250, 3.346878500200758833 ) ) ;
#10231=CARTESIAN_POINT ( 'NONE',  ( 6.196878017913830305, -3.367876570272811509, 4.166666666666666963 ) ) ;
#10250=CONICAL_SURFACE ( 'NONE', #1814, 5.000000000000000000, 1.047197551196600296 ) ;
#10251=ORIENTED_EDGE ( 'NONE', *, *, #8915, .F. ) ;
#10276=EDGE_CURVE ( 'NONE', #4901, #18786, #17248, .T. ) ;
#10284=ADVANCED_FACE ( 'NONE', ( #6049 ), #10648, .T. ) ;
#10291=DIRECTION ( 'NONE',  ( 0.000000000000000000, 0.000000000000000000, -1.000000000000000000 ) ) ;
#10312=ORIENTED_EDGE ( 'NONE', *, *, #766, .T. ) ;
#10323=ORIENTED_EDGE ( 'NONE', *, *, #3817, .T. ) ;
#10342=CARTESIAN_POINT ( 'NONE',  ( -3.574908632038010113E-15, 4.821944789745366222, -1.648146632869000427 ) ) ;
#10351=VECTOR ( 'NONE', #18421, 1000.000000000000000 ) ;
#10359=AXIS2_PLACEMENT_3D ( 'NONE', #2871, #8834, #16191 ) ;
#10363=( NAMED_UNIT ( * ) PLANE_ANGLE_UNIT ( ) SI_UNIT ( $, .RADIAN. ) );
#10386=AXIS2_PLACEMENT_3D ( 'NONE', #10745, #16746, #1837 ) ;
#10412=ADVANCED_FACE ( 'NONE', ( #8145 ), #9409, .F. ) ;
#10414=ORIENTED_EDGE ( 'NONE', *, *, #8782, .F. ) ;
#10440=DIRECTION ( 'NONE',  ( -1.000000000000000000, -0.000000000000000000, -0.000000000000000000 ) ) ;
#10483=CARTESIAN_POINT ( 'NONE',  ( 6.207671477327291853, -3.321994320370684317, 4.246137054662720622 ) ) ;
#10495=CARTESIAN_POINT ( 'NONE',  ( 6.452281807715809059, 2.898928808472990060, 5.021091983800332947 ) ) ;
#10567=CARTESIAN_POINT ( 'NONE',  ( 6.534838248920896930, -2.951765777552406878, 5.112608298763836601 ) ) ;
#10594=CARTESIAN_POINT ( 'NONE',  ( 6.466260427357663154, 2.904280683598005730, 5.030361703432624232 ) ) ;
#10595=CARTESIAN_POINT ( 'NONE',  ( 5.991014884144048480, 2.818925648462311528E-15, 4.999999999999999112 ) ) ;
#10608=CARTESIAN_POINT ( 'NONE',  ( 6.403457969954085449, 2.888443235695447253, -5.002930439003170804 ) ) ;
#10630=CARTESIAN_POINT ( 'NONE',  ( 7.900000000000002132, 0.000000000000000000, 0.000000000000000000 ) ) ;
#10631=ORIENTED_EDGE ( 'NONE', *, *, #6386, .F. ) ;
#10648=CONICAL_SURFACE ( 'NONE', #3770, 5.000000000000000000, 1.047197551196600296 ) ;
#10669=CARTESIAN_POINT ( 'NONE',  ( 6.445127866599364097, -3.194847394660946360, 4.687657648742338701 ) ) ;
#10703=LINE ( 'NONE', #4830, #13787 ) ;
#10736=VERTEX_POINT ( 'NONE', #17409 ) ;
#10742=CARTESIAN_POINT ( 'NONE',  ( 6.371919382990604674, 1.972754410575522588, 5.108792907957607099 ) ) ;
#10745=CARTESIAN_POINT ( 'NONE',  ( 52.80949999999998568, 0.000000000000000000, 0.000000000000000000 ) ) ;
#10770=CARTESIAN_POINT ( 'NONE',  ( -4.878909776184767981E-16, 0.4887495715076933811, 4.999999999999999112 ) ) ;
#10788=CARTESIAN_POINT ( 'NONE',  ( 6.534838248920897819, 2.951765777552412651, 5.112608298763836601 ) ) ;
#10793=CIRCLE ( 'NONE', #6403, 0.5999999999999980904 ) ;
#10799=FACE_OUTER_BOUND ( 'NONE', #19387, .T. ) ;
#10818=EDGE_LOOP ( 'NONE', ( #10027, #11495, #7842, #2334 ) ) ;
#10841=CARTESIAN_POINT ( 'NONE',  ( 6.436591462021358012, -5.789018756751932671, 5.527293451046372024E-16 ) ) ;
#10853=ORIENTED_EDGE ( 'NONE', *, *, #8682, .T. ) ;
#10865=EDGE_LOOP ( 'NONE', ( #8094, #10872, #7407 ) ) ;
#10872=ORIENTED_EDGE ( 'NONE', *, *, #6386, .T. ) ;
#10910=CARTESIAN_POINT ( 'NONE',  ( 6.327632967271008546, -3.313549392874691524, -4.260764098152702850 ) ) ;
#10924=DIRECTION ( 'NONE',  ( 0.000000000000000000, 0.000000000000000000, -1.000000000000000000 ) ) ;
#10943=EDGE_CURVE ( 'NONE', #9923, #10736, #1088, .T. ) ;
#11032=CARTESIAN_POINT ( 'NONE',  ( 6.534224484704327374, -5.901860969583205829, 2.643887195172161483E-14 ) ) ;
#11047=ORIENTED_EDGE ( 'NONE', *, *, #7997, .T. ) ;
#11055=CARTESIAN_POINT ( 'NONE',  ( 6.534838248920897819, 2.951765777552411318, -5.112608298763837489 ) ) ;
#11090=B_SPLINE_CURVE_WITH_KNOTS ( 'NONE', 3,
 ( #4807, #10770, #16770, #3334, #9296, #11145 ),
 .UNSPECIFIED., .F., .F.,
 ( 4, 2, 4 ),
 ( 0.008261945092156346496, 0.009724140865920691962, 0.01118633663968503569 ),
 .UNSPECIFIED. ) ;
#11095=EDGE_CURVE ( 'NONE', #19334, #10178, #8211, .T. ) ;
#11127=CARTESIAN_POINT ( 'NONE',  ( 6.452281807715817941, -2.898928808472988283, 5.021091983800338276 ) ) ;
#11145=CARTESIAN_POINT ( 'NONE',  ( 0.4465819873852002742, 2.886751345948125547, 4.999999999999999112 ) ) ;
#11174=CARTESIAN_POINT ( 'NONE',  ( 6.357976367241631621, 3.426708043487392885, -4.282301071214502208 ) ) ;
#11178=FACE_OUTER_BOUND ( 'NONE', #6590, .T. ) ;
#11189=EDGE_CURVE ( 'NONE', #12590, #13221, #8545, .T. ) ;
#11213=CARTESIAN_POINT ( 'NONE',  ( 6.385552186430389021, -2.886751345948133984, -5.000000000000000000 ) ) ;
#11214=ORIENTED_EDGE ( 'NONE', *, *, #5708, .T. ) ;
#11223=CARTESIAN_POINT ( 'NONE',  ( 6.534224484704323821, -2.950930484791555841, 5.111161529262928660 ) ) ;
#11238=DIRECTION ( 'NONE',  ( 0.3420201433256622736, 1.150791560227853228E-16, 0.9396926207859106484 ) ) ;
#11358=CARTESIAN_POINT ( 'NONE',  ( 6.245824673232988289, 3.903127342724162840, 3.450227696316072734 ) ) ;
#11359=ORIENTED_EDGE ( 'NONE', *, *, #2156, .T. ) ;
#11376=VECTOR ( 'NONE', #16714, 1000.000000000000000 ) ;
#11393=APPLICATION_CONTEXT ( 'automotive_design' ) ;
#11466=CARTESIAN_POINT ( 'NONE',  ( 6.207671477328021048, 3.321994320370322828, -4.246137054663353005 ) ) ;
#11478=DIRECTION ( 'NONE',  ( 0.000000000000000000, 0.000000000000000000, 1.000000000000000000 ) ) ;
#11485=CARTESIAN_POINT ( 'NONE',  ( 0.000000000000000000, 0.000000000000000000, -5.000000000000000000 ) ) ;
#11495=ORIENTED_EDGE ( 'NONE', *, *, #18270, .F. ) ;
#11501=CARTESIAN_POINT ( 'NONE',  ( 8.500000000000000000, 0.000000000000000000, 0.000000000000000000 ) ) ;
#11506=AXIS2_PLACEMENT_3D ( 'NONE', #16095, #5400, #14509 ) ;
#11515=ADVANCED_FACE ( 'NONE', ( #5142 ), #18408, .F. ) ;
#11516=EDGE_LOOP ( 'NONE', ( #17897, #9825, #9018, #14145 ) ) ;
#11529=CARTESIAN_POINT ( 'NONE',  ( 0.08165819712376973238, 4.939961795957293234, 1.443735181952769064 ) ) ;
#11535=B_SPLINE_CURVE_WITH_KNOTS ( 'NONE', 3,
 ( #12605, #6629, #109, #8197, #6088 ),
 .UNSPECIFIED., .F., .F.,
 ( 4, 1, 4 ),
 ( 0.000000000000000000, 0.002886751345948128985, 0.005773502691896257970 ),
 .UNSPECIFIED. ) ;
#11552=TOROIDAL_SURFACE ( 'NONE', #5611, 7.900000000000002132, 0.5999999999999979794 ) ;
#11578=DIRECTION ( 'NONE',  ( -1.000000000000000000, -0.000000000000000000, -0.000000000000000000 ) ) ;
#11591=DIRECTION ( 'NONE',  ( 0.000000000000000000, 0.000000000000000000, 1.000000000000000000 ) ) ;
#11596=ORIENTED_EDGE ( 'NONE', *, *, #4492, .T. ) ;
#11600=CIRCLE ( 'NONE', #17882, 7.900000000000002132 ) ;
#11601=ORIENTED_EDGE ( 'NONE', *, *, #6157, .T. ) ;
#11608=CARTESIAN_POINT ( 'NONE',  ( 8.500000000000000000, 2.886751345948123770, -5.000000000000000000 ) ) ;
#11649=CARTESIAN_POINT ( 'NONE',  ( 6.541171661047875396, 2.934678558896536504, 5.142480235691129664 ) ) ;
#11653=EDGE_CURVE ( 'NONE', #9187, #18339, #15559, .T. ) ;
#11658=CARTESIAN_POINT ( 'NONE',  ( 7.900000000000002132, 9.674709713264094059E-16, -7.900000000000002132 ) ) ;
#11666=CARTESIAN_POINT ( 'NONE',  ( 0.1983443223721553794, -3.359771601077102154, 4.180704885107414448 ) ) ;
#11668=EDGE_LOOP ( 'NONE', ( #3674, #2708, #12493, #17109 ) ) ;
#11680=CARTESIAN_POINT ( 'NONE',  ( 6.367873360227556567, 2.886751345948125991, 4.999999999999999112 ) ) ;
#11720=EDGE_CURVE ( 'NONE', #3828, #18807, #18087, .T. ) ;
#11767=CARTESIAN_POINT ( 'NONE',  ( 6.196878017913830305, 3.367876570272813730, 4.166666666666666075 ) ) ;
#11783=EDGE_CURVE ( 'NONE', #2523, #13933, #7120, .T. ) ;
#11799=CLOSED_SHELL ( 'NONE', ( #13836, #12811, #6739, #2363, #18905, #3428, #18941, #17728, #3590, #14301, #15424, #16736, #10284, #2720, #13948, #13105, #13123, #14581, #9038, #18416, #11515, #19139, #3182, #18183, #18736, #18883, #14287, #9737, #10412 ) ) ;
#11830=DIRECTION ( 'NONE',  ( -1.000000000000000000, -0.000000000000000000, -0.000000000000000000 ) ) ;
#11919=CONICAL_SURFACE ( 'NONE', #7225, 3.309499999999999886, 0.7853981633974407295 ) ;
#11934=DIRECTION ( 'NONE',  ( 1.000000000000000000, 0.000000000000000000, -0.000000000000000000 ) ) ;
#11939=VERTEX_POINT ( 'NONE', #7676 ) ;
#11947=CARTESIAN_POINT ( 'NONE',  ( 6.481779955677436256, 5.820445026626583918, -1.884471986315529758E-16 ) ) ;
#11955=DIRECTION ( 'NONE',  ( -0.000000000000000000, 1.000000000000000000, 1.224646799147353207E-16 ) ) ;
#12058=CARTESIAN_POINT ( 'NONE',  ( 6.362374563307726660, -5.433808049138435514, 0.8060918076010795685 ) ) ;
#12061=DIRECTION ( 'NONE',  ( 0.000000000000000000, 0.000000000000000000, -1.000000000000000000 ) ) ;
#12066=B_SPLINE_CURVE_WITH_KNOTS ( 'NONE', 3,
 ( #12933, #18938, #5477, #1666, #14885, #16756, #1356, #11947, #4510, #6161, #8904, #9193, #16566, #5979, #13522, #3324 ),
 .UNSPECIFIED., .F., .F.,
 ( 4, 3, 3, 3, 3, 4 ),
 ( 0.000000000000000000, 5.303647860849293065E-05, 0.0001057093501027226378, 0.0001642058037231607288, 0.0002210073443958831293, 0.0002236769549542879461 ),
 .UNSPECIFIED. ) ;
#12069=CARTESIAN_POINT ( 'NONE',  ( 6.534838248920897819, 2.951765777552412651, 5.112608298763836601 ) ) ;
#12102=CARTESIAN_POINT ( 'NONE',  ( 6.207519134555854023, 1.039264565631282888, -4.999999999999109157 ) ) ;
#12122=( NAMED_UNIT ( * ) SI_UNIT ( $, .STERADIAN. ) SOLID_ANGLE_UNIT ( ) );
#12128=CARTESIAN_POINT ( 'NONE',  ( 7.900000000000002132, 0.000000000000000000, 0.000000000000000000 ) ) ;
#12156=FACE_OUTER_BOUND ( 'NONE', #3917, .T. ) ;
#12224=CARTESIAN_POINT ( 'NONE',  ( 6.420058897733094128, -5.782965130189196223, 5.134498127650324400E-16 ) ) ;
#12228=FACE_OUTER_BOUND ( 'NONE', #14531, .T. ) ;
#12259=EDGE_CURVE ( 'NONE', #11939, #17113, #843, .T. ) ;
#12272=CARTESIAN_POINT ( 'NONE',  ( 6.445127866599366762, 5.657054305385774917, 0.4229901806197435277 ) ) ;
#12317=CARTESIAN_POINT ( 'NONE',  ( 6.385552186430389909, -5.773502691896263528, -1.564818079814629131E-31 ) ) ;
#12336=CARTESIAN_POINT ( 'NONE',  ( 0.01055556052338940676, 4.084588180558400339, -2.925285743277528105 ) ) ;
#12339=CARTESIAN_POINT ( 'NONE',  ( 6.270568613849413886, 3.932080789230360196, -3.401571648088637101 ) ) ;
#12394=EDGE_CURVE ( 'NONE', #3064, #9923, #1992, .T. ) ;
#12401=ORIENTED_EDGE ( 'NONE', *, *, #15391, .F. ) ;
#12411=CARTESIAN_POINT ( 'NONE',  ( 6.466260427357665819, -5.808561367196025671, 1.503437176544561004E-15 ) ) ;
#12421=VERTEX_POINT ( 'NONE', #1397 ) ;
#12426=DIRECTION ( 'NONE',  ( 0.000000000000000000, 0.000000000000000000, -1.000000000000000000 ) ) ;
#12462=CARTESIAN_POINT ( 'NONE',  ( 6.481779955677444249, 2.910222513313288850, -5.040653254389421356 ) ) ;
#12476=( GEOMETRIC_REPRESENTATION_CONTEXT ( 3 ) GLOBAL_UNCERTAINTY_ASSIGNED_CONTEXT ( ( #19339 ) ) GLOBAL_UNIT_ASSIGNED_CONTEXT ( ( #8900, #5573, #2752 ) ) REPRESENTATION_CONTEXT ( 'NONE', 'WORKASPACE' ) );
#12481=CARTESIAN_POINT ( 'NONE',  ( 6.245813541929285506, 1.036329910265332499, -5.105320956836708390 ) ) ;
#12492=CARTESIAN_POINT ( 'NONE',  ( 6.534838248920899595, -2.951765777552420644, -5.112608298763837489 ) ) ;
#12493=ORIENTED_EDGE ( 'NONE', *, *, #11720, .F. ) ;
#12527=ORIENTED_EDGE ( 'NONE', *, *, #167, .F. ) ;
#12541=CARTESIAN_POINT ( 'NONE',  ( 0.4465819873852039379, 5.773502691896261751, 3.331019006688249527E-17 ) ) ;
#12566=VECTOR ( 'NONE', #5108, 1000.000000000000000 ) ;
#12590=VERTEX_POINT ( 'NONE', #19033 ) ;
#12605=CARTESIAN_POINT ( 'NONE',  ( 6.367873360227558344, -2.886751345948133984, -5.000000000000000000 ) ) ;
#12608=PRODUCT_DEFINITION_FORMATION_WITH_SPECIFIED_SOURCE ( 'ANY', '', #12728, .NOT_KNOWN. ) ;
#12615=VERTEX_POINT ( 'NONE', #4206 ) ;
#12633=EDGE_CURVE ( 'NONE', #17668, #12590, #13378, .T. ) ;
#12658=CARTESIAN_POINT ( 'NONE',  ( 6.095473853218515536, 4.853892138986921623, -1.592812200815479695 ) ) ;
#12680=CARTESIAN_POINT ( 'NONE',  ( 6.095484975317565279, -1.047622383848427985, 4.999999999999999112 ) ) ;
#12692=CARTESIAN_POINT ( 'NONE',  ( 6.403457969954082785, -2.888443235695457467, -5.002930439003169916 ) ) ;
#12704=FACE_OUTER_BOUND ( 'NONE', #9288, .T. ) ;
#12728=PRODUCT ( 'hex flange bolt small_iso_ISO 4162 - M8 x 45 x 22-N', 'hex flange bolt small_iso_ISO 4162 - M8 x 45 x 22-N', '', ( #490 ) ) ;
#12768=VERTEX_POINT ( 'NONE', #4829 ) ;
#12779=FACE_BOUND ( 'NONE', #14448, .T. ) ;
#12811=ADVANCED_FACE ( 'NONE', ( #1193 ), #14006, .T. ) ;
#12813=CARTESIAN_POINT ( 'NONE',  ( 0.000000000000000000, 4.898587196589412829E-16, -4.000000000000000000 ) ) ;
#12820=CARTESIAN_POINT ( 'NONE',  ( 7.336184427528458230, 9.926022037524705097E-16, 8.105212085995399107 ) ) ;
#12845=AXIS2_PLACEMENT_3D ( 'NONE', #2840, #11934, #17649 ) ;
#12863=EDGE_CURVE ( 'NONE', #13093, #7769, #6204, .T. ) ;
#12886=ORIENTED_EDGE ( 'NONE', *, *, #17545, .T. ) ;
#12910=CARTESIAN_POINT ( 'NONE',  ( 0.000000000000000000, 5.773502691896261751, -2.749426538070115714E-16 ) ) ;
#12921=CARTESIAN_POINT ( 'NONE',  ( 6.534838248920899595, 5.903531555104835071, 8.098083288904839678E-18 ) ) ;
#12933=CARTESIAN_POINT ( 'NONE',  ( 6.367873360227558344, 5.773502691896261751, 0.000000000000000000 ) ) ;
#12965=VECTOR ( 'NONE', #14617, 1000.000000000000000 ) ;
#12967=CARTESIAN_POINT ( 'NONE',  ( 6.092439126518621073, 1.005559546149547678, 4.999999999999999112 ) ) ;
#12979=CARTESIAN_POINT ( 'NONE',  ( 1.753358200816401209E-16, -0.4883827417527520920, -4.999999999999999112 ) ) ;
#12993=CARTESIAN_POINT ( 'NONE',  ( 6.367873360227558344, -2.886751345948133984, -5.000000000000000000 ) ) ;
#13007=VERTEX_POINT ( 'NONE', #4622 ) ;
#13010=ORIENTED_EDGE ( 'NONE', *, *, #79, .F. ) ;
#13029=CARTESIAN_POINT ( 'NONE',  ( 6.362374563307939823, 3.415000007733389076, 4.302769906042884784 ) ) ;
#13036=APPLICATION_CONTEXT ( 'automotive_design' ) ;
#13071=ORIENTED_EDGE ( 'NONE', *, *, #3762, .T. ) ;
#13091=DIRECTION ( 'NONE',  ( 0.000000000000000000, 0.8660254037844375974, -0.5000000000000018874 ) ) ;
#13093=VERTEX_POINT ( 'NONE', #112 ) ;
#13105=ADVANCED_FACE ( 'NONE', ( #1481 ), #10250, .T. ) ;
#13123=ADVANCED_FACE ( 'NONE', ( #12156 ), #270, .T. ) ;
#13128=CARTESIAN_POINT ( 'NONE',  ( 6.327632967268630004, 3.313549392874629795, 4.260764098153893897 ) ) ;
#13166=DIRECTION ( 'NONE',  ( -1.000000000000000000, -0.000000000000000000, -0.000000000000000000 ) ) ;
#13175=AXIS2_PLACEMENT_3D ( 'NONE', #1406, #9140, #2080 ) ;
#13179=CARTESIAN_POINT ( 'NONE',  ( 0.04201760816084261496, -0.9730571234389092661, -5.000000000000000888 ) ) ;
#13185=CARTESIAN_POINT ( 'NONE',  ( 6.196878017913831194, -5.292377467571572680, 0.8333333333333327042 ) ) ;
#13221=VERTEX_POINT ( 'NONE', #12541 ) ;
#13245=ORIENTED_EDGE ( 'NONE', *, *, #4436, .F. ) ;
#13251=CARTESIAN_POINT ( 'NONE',  ( 6.527192678185834041, 2.941622124011172623, 5.095038975455953079 ) ) ;
#13263=ORIENTED_EDGE ( 'NONE', *, *, #17698, .F. ) ;
#13270=EDGE_CURVE ( 'NONE', #2819, #12421, #19278, .T. ) ;
#13275=PLANE ( 'NONE',  #15778 ) ;
#13287=ORIENTED_EDGE ( 'NONE', *, *, #4492, .F. ) ;
#13323=CARTESIAN_POINT ( 'NONE',  ( 0.08165819712377191120, -4.939961795957299451, -1.443735181952766400 ) ) ;
#13351=AXIS2_PLACEMENT_3D ( 'NONE', #15419, #8053, #4929 ) ;
#13375=CARTESIAN_POINT ( 'NONE',  ( -1.575481281892997891E-16, 0.4887495715076908831, -5.000000000000000000 ) ) ;
#13378=CIRCLE ( 'NONE', #4923, 4.999999999999999112 ) ;
#13405=CARTESIAN_POINT ( 'NONE',  ( 6.367873360227556567, 2.886751345948123770, -5.000000000000000000 ) ) ;
#13422=EDGE_LOOP ( 'NONE', ( #17700, #19192, #19039, #8807 ) ) ;
#13428=SHAPE_REPRESENTATION ( 'hex flange bolt small_iso_ISO 4162 - M8 x 45 x 22-N', ( #10359 ), #1541 ) ;
#13455=EDGE_CURVE ( 'NONE', #17828, #17145, #14192, .T. ) ;
#13468=CARTESIAN_POINT ( 'NONE',  ( 6.367873360227558344, 5.773502691896261751, 0.000000000000000000 ) ) ;
#13480=EDGE_CURVE ( 'NONE', #13933, #13007, #15010, .T. ) ;
#13506=CARTESIAN_POINT ( 'NONE',  ( 6.445379721942638973, 2.463581311471617852, 5.110653333236676588 ) ) ;
#13513=AXIS2_PLACEMENT_3D ( 'NONE', #4951, #10924, #736 ) ;
#13522=CARTESIAN_POINT ( 'NONE',  ( 6.534533895392296010, 5.902695350657467088, 5.075181882648644095E-15 ) ) ;
#13537=CARTESIAN_POINT ( 'NONE',  ( 6.507056315241511513, -2.833450876375909644, 5.092319121366346124 ) ) ;
#13547=CARTESIAN_POINT ( 'NONE',  ( 6.506987859255518813, 2.925375531177291766, 5.066899051217865768 ) ) ;
#13564=CARTESIAN_POINT ( 'NONE',  ( 53.50000000000000000, 0.000000000000000000, 0.000000000000000000 ) ) ;
#13635=DIRECTION ( 'NONE',  ( 0.000000000000000000, 0.000000000000000000, -1.000000000000000000 ) ) ;
#13645=CARTESIAN_POINT ( 'NONE',  ( 6.534838248920900483, -5.903531555104836848, 4.671345613696493211E-16 ) ) ;
#13653=CARTESIAN_POINT ( 'NONE',  ( 6.534533895392294234, 2.951347675328729991, -5.111884124469655788 ) ) ;
#13671=DIRECTION ( 'NONE',  ( -1.000000000000000000, -0.000000000000000000, -0.000000000000000000 ) ) ;
#13689=DIRECTION ( 'NONE',  ( 0.000000000000000000, 0.000000000000000000, 1.000000000000000000 ) ) ;
#13690=CARTESIAN_POINT ( 'NONE',  ( 6.534838248920900483, -5.903531555104836848, 4.671345613696493211E-16 ) ) ;
#13752=EDGE_LOOP ( 'NONE', ( #774, #5256, #6905, #13010, #18819 ) ) ;
#13758=CARTESIAN_POINT ( 'NONE',  ( 0.000000000000000000, 0.000000000000000000, -5.000000000000000000 ) ) ;
#13767=CARTESIAN_POINT ( 'NONE',  ( 6.207660606243411650, -2.016205878028328957, -5.000000000000000000 ) ) ;
#13787=VECTOR ( 'NONE', #7952, 999.9999999999998863 ) ;
#13791=ORIENTED_EDGE ( 'NONE', *, *, #167, .T. ) ;
#13802=ORIENTED_EDGE ( 'NONE', *, *, #11720, .T. ) ;
#13808=CARTESIAN_POINT ( 'NONE',  ( 0.000000000000000000, 0.000000000000000000, 0.000000000000000000 ) ) ;
#13836=ADVANCED_FACE ( 'NONE', ( #12228 ), #7167, .T. ) ;
#13841=ORIENTED_EDGE ( 'NONE', *, *, #17298, .F. ) ;
#13842=CARTESIAN_POINT ( 'NONE',  ( 6.452281807715818829, 2.898928808472990948, -5.021091983800339165 ) ) ;
#13915=CARTESIAN_POINT ( 'NONE',  ( 6.534838248920899595, 5.903531555104835071, 8.098083288904839678E-18 ) ) ;
#13933=VERTEX_POINT ( 'NONE', #2435 ) ;
#13944=CARTESIAN_POINT ( 'NONE',  ( 6.204460410672267834, -4.828986228461502606, -1.635950503254466337 ) ) ;
#13948=ADVANCED_FACE ( 'NONE', ( #15658 ), #588, .T. ) ;
#13950=CARTESIAN_POINT ( 'NONE',  ( 6.541171952014627422, 2.986180817377861896, -5.112746308113085725 ) ) ;
#14006=CONICAL_SURFACE ( 'NONE', #11506, 8.105212085995399107, 1.221730476396037490 ) ;
#14035=B_SPLINE_CURVE_WITH_KNOTS ( 'NONE', 3,
 ( #8470, #14343, #15929, #1032 ),
 .UNSPECIFIED., .F., .F.,
 ( 4, 4 ),
 ( 0.002977824986803813152, 0.005972417098209346735 ),
 .UNSPECIFIED. ) ;
#14056=CARTESIAN_POINT ( 'NONE',  ( 6.481779955677435368, -2.910222513313295511, -5.040653254389411586 ) ) ;
#14062=DIRECTION ( 'NONE',  ( 0.000000000000000000, -1.000000000000000000, 0.000000000000000000 ) ) ;
#14068=CARTESIAN_POINT ( 'NONE',  ( 6.533910050139697390, -5.901028503456124064, 1.992084869049455159E-14 ) ) ;
#14102=CARTESIAN_POINT ( 'NONE',  ( 6.244297270355322560, -0.4917101305082151597, -5.105276777067913052 ) ) ;
#14109=CARTESIAN_POINT ( 'NONE',  ( 0.4465819873851989974, -2.886751345948120218, 4.999999999999999112 ) ) ;
#14145=ORIENTED_EDGE ( 'NONE', *, *, #17545, .F. ) ;
#14174=LINE ( 'NONE', #12813, #3724 ) ;
#14192=LINE ( 'NONE', #4012, #7463 ) ;
#14204=CARTESIAN_POINT ( 'NONE',  ( 6.534838248920897819, 2.951765777552411318, -5.112608298763837489 ) ) ;
#14222=AXIS2_PLACEMENT_3D ( 'NONE', #8243, #18759, #3745 ) ;
#14227=CARTESIAN_POINT ( 'NONE',  ( -2.915605589912154091E-15, 3.838309248099015747, 3.351853367131007566 ) ) ;
#14254=AXIS2_PLACEMENT_3D ( 'NONE', #15372, #1952, #2142 ) ;
#14271=ORIENTED_EDGE ( 'NONE', *, *, #8915, .T. ) ;
#14287=ADVANCED_FACE ( 'NONE', ( #3486 ), #2681, .F. ) ;
#14301=ADVANCED_FACE ( 'NONE', ( #1923 ), #11552, .T. ) ;
#14340=ORIENTED_EDGE ( 'NONE', *, *, #5676, .T. ) ;
#14343=CARTESIAN_POINT ( 'NONE',  ( 6.244297270353399654, -0.9889575675955545320, 5.105276777067856209 ) ) ;
#14357=CARTESIAN_POINT ( 'NONE',  ( 5.991014884144047592, -4.330127018922191873, 2.499999999999998668 ) ) ;
#14380=B_SPLINE_CURVE_WITH_KNOTS ( 'NONE', 3,
 ( #11680, #16403, #4536, #3072, #3169, #10495, #10594, #2970, #15115, #13547, #1491, #13251, #5805, #7467, #120, #12069 ),
 .UNSPECIFIED., .F., .F.,
 ( 4, 3, 3, 3, 3, 4 ),
 ( 0.000000000000000000, 5.303647860849292387E-05, 0.0001057093501027219331, 0.0001642058037231606204, 0.0002210073443958821807, 0.0002236769549542877021 ),
 .UNSPECIFIED. ) ;
#14417=B_SPLINE_CURVE_WITH_KNOTS ( 'NONE', 3,
 ( #13915, #12272, #17176, #6572, #18368, #4915, #3735, #10788 ),
 .UNSPECIFIED., .F., .F.,
 ( 4, 2, 2, 4 ),
 ( 0.000000000000000000, 0.001493104274552339720, 0.002986208549104679439, 0.005972417098209361480 ),
 .UNSPECIFIED. ) ;
#14447=MECHANICAL_DESIGN_GEOMETRIC_PRESENTATION_REPRESENTATION('',(#19185),#1318);
#14448=EDGE_LOOP ( 'NONE', ( #13802, #14512 ) ) ;
#14457=ORIENTED_EDGE ( 'NONE', *, *, #3350, .F. ) ;
#14467=CARTESIAN_POINT ( 'NONE',  ( 6.534533895392292457, -2.951347675328713116, 5.111884124469662893 ) ) ;
#14480=EDGE_LOOP ( 'NONE', ( #17193, #1953, #18394, #3866 ) ) ;
#14509=DIRECTION ( 'NONE',  ( 0.000000000000000000, 0.000000000000000000, -1.000000000000000000 ) ) ;
#14512=ORIENTED_EDGE ( 'NONE', *, *, #17298, .T. ) ;
#14531=EDGE_LOOP ( 'NONE', ( #7507, #9196, #7691, #4621 ) ) ;
#14537=EDGE_LOOP ( 'NONE', ( #12401, #1749, #13071, #13841 ) ) ;
#14569=CARTESIAN_POINT ( 'NONE',  ( 0.01055556052338981095, 4.575665857285978078, 2.074714256722482997 ) ) ;
#14576=CARTESIAN_POINT ( 'NONE',  ( 53.50000000000000000, 0.000000000000000000, 3.309499999999999886 ) ) ;
#14581=ADVANCED_FACE ( 'NONE', ( #10124 ), #4347, .F. ) ;
#14600=LINE ( 'NONE', #1090, #9083 ) ;
#14617=DIRECTION ( 'NONE',  ( -1.000000000000000000, -0.000000000000000000, -0.000000000000000000 ) ) ;
#14635=DIRECTION ( 'NONE',  ( 0.000000000000000000, 0.000000000000000000, -1.000000000000000000 ) ) ;
#14680=CARTESIAN_POINT ( 'NONE',  ( 6.244297270354684848, -1.798312406574552930E-11, -5.105276777067894400 ) ) ;
#14691=AXIS2_PLACEMENT_3D ( 'NONE', #5725, #19187, #16029 ) ;
#14696=CARTESIAN_POINT ( 'NONE',  ( 0.1983443223721600701, -5.300482436767282479, -0.8192951148925879945 ) ) ;
#14716=CARTESIAN_POINT ( 'NONE',  ( 6.196878017913833858, 5.292377467571573568, 0.8333333333333322601 ) ) ;
#14760=VECTOR ( 'NONE', #5396, 1000.000000000000114 ) ;
#14778=PRODUCT_DEFINITION_SHAPE ( 'NONE', 'NONE',  #8787 ) ;
#14817=CARTESIAN_POINT ( 'NONE',  ( 6.367873360227558344, 5.773502691896261751, 0.000000000000000000 ) ) ;
#14885=CARTESIAN_POINT ( 'NONE',  ( 6.436591462021357124, 5.789018756751930894, -2.883547477572278442E-16 ) ) ;
#14904=CARTESIAN_POINT ( 'NONE',  ( 0.1739375980333740523, -5.301268757141563093, 0.8179331680533010740 ) ) ;
#15000=CARTESIAN_POINT ( 'NONE',  ( 6.212068001624178493, -5.350125758160219291, 0.7333103599835463227 ) ) ;
#15010=B_SPLINE_CURVE_WITH_KNOTS ( 'NONE', 3,
 ( #7531, #16371, #3033, #91 ),
 .UNSPECIFIED., .F., .F.,
 ( 4, 4 ),
 ( 2.380735203086575858E-07, 0.002921158011986710323 ),
 .UNSPECIFIED. ) ;
#15026=CARTESIAN_POINT ( 'NONE',  ( 53.50000000000000000, 0.000000000000000000, 0.000000000000000000 ) ) ;
#15046=CARTESIAN_POINT ( 'NONE',  ( 0.4465819873852006072, 2.886751345948123770, -5.000000000000000000 ) ) ;
#15058=CARTESIAN_POINT ( 'NONE',  ( 6.204471256525345702, -0.9979289516723606202, -5.000000000000889955 ) ) ;
#15091=B_SPLINE_CURVE_WITH_KNOTS ( 'NONE', 3,
 ( #15840, #13185, #14357, #10231, #2529 ),
 .UNSPECIFIED., .F., .F.,
 ( 4, 1, 4 ),
 ( 9.359404341228126911E-20, 0.002886751345948132021, 0.005773502691896264041 ),
 .UNSPECIFIED. ) ;
#15107=ORIENTED_EDGE ( 'NONE', *, *, #13270, .F. ) ;
#15108=CARTESIAN_POINT ( 'NONE',  ( 0.000000000000000000, 0.000000000000000000, 0.000000000000000000 ) ) ;
#15113=FACE_OUTER_BOUND ( 'NONE', #4260, .T. ) ;
#15115=CARTESIAN_POINT ( 'NONE',  ( 6.495567275915077765, 2.917443832164883233, 5.053160945538031079 ) ) ;
#15127=ORIENTED_EDGE ( 'NONE', *, *, #18171, .T. ) ;
#15133=CYLINDRICAL_SURFACE ( 'NONE', #18295, 4.000000000000000000 ) ;
#15142=CARTESIAN_POINT ( 'NONE',  ( 6.092449800118536096, -4.833012432206597708, -1.628976913806147397 ) ) ;
#15147=CARTESIAN_POINT ( 'NONE',  ( 6.541333988313477121, -2.987057409892287740, -5.112749828287758369 ) ) ;
#15168=CARTESIAN_POINT ( 'NONE',  ( 6.196878017913833858, -1.924500897298759172, -5.000000000000000888 ) ) ;
#15173=DIRECTION ( 'NONE',  ( -1.000000000000000000, -0.000000000000000000, -0.000000000000000000 ) ) ;
#15188=CARTESIAN_POINT ( 'NONE',  ( 0.3106000600989267113, 3.122278952918445150, -4.592054218142293642 ) ) ;
#15235=CARTESIAN_POINT ( 'NONE',  ( 6.242800618755285136, -4.918813924287352535, -1.690830708135802052 ) ) ;
#15280=B_SPLINE_CURVE_WITH_KNOTS ( 'NONE', 3,
 ( #1641, #7217, #10342, #5749 ),
 .UNSPECIFIED., .F., .F.,
 ( 4, 4 ),
 ( 2.380735200831296902E-07, 0.002921158011986723767 ),
 .UNSPECIFIED. ) ;
#15284=CARTESIAN_POINT ( 'NONE',  ( 0.4465819873852006072, 2.886751345948123770, -5.000000000000000000 ) ) ;
#15294=B_SPLINE_CURVE_WITH_KNOTS ( 'NONE', 3,
 ( #4049, #5507, #14227, #3854 ),
 .UNSPECIFIED., .F., .F.,
 ( 4, 4 ),
 ( 2.380735200829041677E-07, 0.002921158011986707288 ),
 .UNSPECIFIED. ) ;
#15296=SHAPE_DEFINITION_REPRESENTATION ( #14778, #13428 ) ;
#15308=LINE ( 'NONE', #18566, #12566 ) ;
#15320=CARTESIAN_POINT ( 'NONE',  ( 6.466260427357672924, 2.904280683598007951, -5.030361703432632225 ) ) ;
#15359=DIRECTION ( 'NONE',  ( -1.000000000000000000, -0.000000000000000000, -0.000000000000000000 ) ) ;
#15372=CARTESIAN_POINT ( 'NONE',  ( 7.336184427528458230, 0.000000000000000000, 0.000000000000000000 ) ) ;
#15376=CARTESIAN_POINT ( 'NONE',  ( 0.000000000000000000, 0.000000000000000000, 0.000000000000000000 ) ) ;
#15380=CARTESIAN_POINT ( 'NONE',  ( 0.05140428708382594608, 3.841181488860376358, -3.346878500200759277 ) ) ;
#15391=EDGE_CURVE ( 'NONE', #11939, #18807, #14174, .T. ) ;
#15419=CARTESIAN_POINT ( 'NONE',  ( 0.000000000000000000, 0.000000000000000000, 0.000000000000000000 ) ) ;
#15424=ADVANCED_FACE ( 'NONE', ( #2439 ), #3803, .F. ) ;
#15478=CARTESIAN_POINT ( 'NONE',  ( 0.000000000000000000, 0.000000000000000000, 5.000000000000000000 ) ) ;
#15539=CARTESIAN_POINT ( 'NONE',  ( 6.495567275915079541, -2.917443832164891226, -5.053160945538031967 ) ) ;
#15559=B_SPLINE_CURVE_WITH_KNOTS ( 'NONE', 3,
 ( #12492, #18603, #18504, #8080, #17029, #7797, #3585, #15539, #14056, #638, #6615, #8180, #9644, #12692, #11213, #17219 ),
 .UNSPECIFIED., .F., .F.,
 ( 4, 3, 3, 3, 3, 4 ),
 ( -2.669610558406318528E-06, 0.000000000000000000, 5.703179328867203279E-05, 0.0001157653700806028548, 0.0001686517580799736817, 0.0002219032271235106112 ),
 .UNSPECIFIED. ) ;
#15572=CARTESIAN_POINT ( 'NONE',  ( 0.000000000000000000, 4.330127018922190096, -2.500000000000006217 ) ) ;
#15607=COLOUR_RGB ( '',1.000000000000000000, 0.9490196078431372140, 0.9098039215686274384 ) ;
#15626=CARTESIAN_POINT ( 'NONE',  ( 6.507056549636238252, 2.993353539201078828, 4.999999999999999112 ) ) ;
#15639=ORIENTED_EDGE ( 'NONE', *, *, #340, .T. ) ;
#15654=CARTESIAN_POINT ( 'NONE',  ( 6.323279575526007612, -3.325091652217148308, 4.240772318536393470 ) ) ;
#15658=FACE_OUTER_BOUND ( 'NONE', #5918, .T. ) ;
#15672=DIRECTION ( 'NONE',  ( -1.000000000000000000, -0.000000000000000000, -0.000000000000000000 ) ) ;
#15727=ORIENTED_EDGE ( 'NONE', *, *, #18219, .F. ) ;
#15778=AXIS2_PLACEMENT_3D ( 'NONE', #11608, #18898, #1226 ) ;
#15791=CARTESIAN_POINT ( 'NONE',  ( 6.355324643801638196, 1.972141403783284730, -5.108685331087993831 ) ) ;
#15800=CARTESIAN_POINT ( 'NONE',  ( 6.327632967270859332, 5.346704644972003706, -0.7392359018481428068 ) ) ;
#15824=PLANE ( 'NONE',  #16941 ) ;
#15840=CARTESIAN_POINT ( 'NONE',  ( 6.367873360227559232, -5.773502691896263528, 0.000000000000000000 ) ) ;
#15871=EDGE_CURVE ( 'NONE', #19334, #1202, #14035, .T. ) ;
#15882=CARTESIAN_POINT ( 'NONE',  ( 6.207671477328661425, 5.338259717474330479, 0.7538629453361838095 ) ) ;
#15929=CARTESIAN_POINT ( 'NONE',  ( 6.355324643801635531, -1.972141403783270075, 5.108685331087992942 ) ) ;
#15944=CARTESIAN_POINT ( 'NONE',  ( 6.506987859255527695, -2.925375531177290878, 5.066899051217877314 ) ) ;
#15974=DIRECTION ( 'NONE',  ( -1.000000000000000000, -0.000000000000000000, -0.000000000000000000 ) ) ;
#16005=AXIS2_PLACEMENT_3D ( 'NONE', #5103, #6853, #18847 ) ;
#16024=CARTESIAN_POINT ( 'NONE',  ( 6.362382503762741948, -2.018850626433581041, 5.108861885121540602 ) ) ;
#16029=DIRECTION ( 'NONE',  ( 1.000000000000000000, 0.000000000000000000, 0.000000000000000000 ) ) ;
#16074=( BOUNDED_SURFACE ( )  B_SPLINE_SURFACE ( 3, 2, ( 
 ( #8526, #1078, #11649 ),
 ( #18845, #13128, #13029 ),
 ( #4209, #10176, #11358 ),
 ( #17363, #3924, #16176 ),
 ( #15882, #4116, #2756 ),
 ( #8712, #984, #7048 ) ),
 .UNSPECIFIED., .F., .F., .T. ) 
 B_SPLINE_SURFACE_WITH_KNOTS ( ( 4, 2, 4 ),
 ( 3, 3 ),
 ( 0.02367865728600889244, 0.02663179453327095547, 0.02958493178053301503 ),
 ( 0.000000000000000000, 1.000000000000000000 ),
 .UNSPECIFIED. ) 
 GEOMETRIC_REPRESENTATION_ITEM ( )  RATIONAL_B_SPLINE_SURFACE ( (
 ( 1.000000000000000000, 0.8047781103519378032, 1.000000000000000000),
 ( 1.000000000000000000, 0.8123785825977077879, 1.000000000000000000),
 ( 1.000000000000000000, 0.8190671539292031511, 1.000000000000000000),
 ( 1.000000000000000000, 0.8192352255331103450, 1.000000000000000000),
 ( 1.000000000000000000, 0.8126129676838903526, 1.000000000000000000),
 ( 1.000000000000000000, 0.8047712537969723412, 1.000000000000000000) ) ) 
 REPRESENTATION_ITEM ( '' )  SURFACE ( )  );
#16078=FILL_AREA_STYLE ('',( #19330 ) ) ;
#16094=CARTESIAN_POINT ( 'NONE',  ( 0.3106000600989247684, -3.122278952918441597, 4.592054218142290978 ) ) ;
#16095=CARTESIAN_POINT ( 'NONE',  ( 7.336184427528458230, 0.000000000000000000, 0.000000000000000000 ) ) ;
#16111=EDGE_CURVE ( 'NONE', #12615, #10736, #1271, .T. ) ;
#16176=CARTESIAN_POINT ( 'NONE',  ( 6.242800618755108388, 4.918813924286816963, 1.690830708135752758 ) ) ;
#16182=CARTESIAN_POINT ( 'NONE',  ( 0.01055556052339245120, -4.575665857285984295, -2.074714256722479888 ) ) ;
#16191=DIRECTION ( 'NONE',  ( 1.000000000000000000, 0.000000000000000000, 0.000000000000000000 ) ) ;
#16239=ORIENTED_EDGE ( 'NONE', *, *, #6157, .F. ) ;
#16270=( LENGTH_UNIT ( ) NAMED_UNIT ( * ) SI_UNIT ( .MILLI., .METRE. ) );
#16274=B_SPLINE_CURVE_WITH_KNOTS ( 'NONE', 3,
 ( #4419, #9009, #16182, #2762, #13323, #14696, #16286, #4517 ),
 .UNSPECIFIED., .F., .F.,
 ( 4, 2, 2, 4 ),
 ( 0.002921158011986710323, 0.003648658599403064445, 0.004376159186819419435, 0.005831160361652128546 ),
 .UNSPECIFIED. ) ;
#16286=CARTESIAN_POINT ( 'NONE',  ( 0.3106000600989309857, -5.537975084925943037, -0.4079457818577079120 ) ) ;
#16305=CARTESIAN_POINT ( 'NONE',  ( 5.991014884144048480, 4.330127018922193649, 2.500000000000001776 ) ) ;
#16326=EDGE_LOOP ( 'NONE', ( #9102, #9537, #16849, #4527, #15639, #11601, #14340 ) ) ;
#16330=FACE_OUTER_BOUND ( 'NONE', #14537, .T. ) ;
#16348=DIRECTION ( 'NONE',  ( 0.000000000000000000, 0.000000000000000000, 1.000000000000000000 ) ) ;
#16371=CARTESIAN_POINT ( 'NONE',  ( 0.1739375980333479343, -3.358985280702903253, -4.182066831946573693 ) ) ;
#16403=CARTESIAN_POINT ( 'NONE',  ( 6.385552186430388133, 2.886751345948125991, 4.999999999999999112 ) ) ;
#16427=DIRECTION ( 'NONE',  ( 0.000000000000000000, 0.000000000000000000, 1.000000000000000000 ) ) ;
#16486=CARTESIAN_POINT ( 'NONE',  ( 6.357976367241810145, -3.426708043488799760, 4.282301071214263288 ) ) ;
#16544=AXIS2_PLACEMENT_3D ( 'NONE', #17378, #7065, #2482 ) ;
#16566=CARTESIAN_POINT ( 'NONE',  ( 6.533910050139697390, 5.901028503456123175, 1.520834953648585461E-14 ) ) ;
#16597=CARTESIAN_POINT ( 'NONE',  ( 6.196878017913834746, 1.924500897298752955, 5.000000000000000000 ) ) ;
#16644=AXIS2_PLACEMENT_3D ( 'NONE', #13564, #16803, #4652 ) ;
#16657=CARTESIAN_POINT ( 'NONE',  ( 0.000000000000000000, 0.000000000000000000, 0.000000000000000000 ) ) ;
#16714=DIRECTION ( 'NONE',  ( -1.000000000000000000, -0.000000000000000000, -0.000000000000000000 ) ) ;
#16736=ADVANCED_FACE ( 'NONE', ( #15113 ), #9697, .T. ) ;
#16743=CARTESIAN_POINT ( 'NONE',  ( 6.244297270354683960, 1.802013835206515036E-11, 5.105276777067893512 ) ) ;
#16746=DIRECTION ( 'NONE',  ( -1.000000000000000000, -0.000000000000000000, -0.000000000000000000 ) ) ;
#16756=CARTESIAN_POINT ( 'NONE',  ( 6.452281807715811723, 5.797857616945992554, -1.918911630784297550E-16 ) ) ;
#16770=CARTESIAN_POINT ( 'NONE',  ( 0.04320752586819863461, 0.9836842030436160345, 4.999999999999999112 ) ) ;
#16803=DIRECTION ( 'NONE',  ( -1.000000000000000000, 0.000000000000000000, -0.000000000000000000 ) ) ;
#16839=CARTESIAN_POINT ( 'NONE',  ( 6.271006797790669829, 0.9853839345309320930, 5.106080050406710313 ) ) ;
#16849=ORIENTED_EDGE ( 'NONE', *, *, #9992, .T. ) ;
#16879=CARTESIAN_POINT ( 'NONE',  ( 6.371919382990606451, -1.972754410575515704, -5.108792907957607099 ) ) ;
#16893=AXIS2_PLACEMENT_3D ( 'NONE', #12910, #8391, #4091 ) ;
#16902=CARTESIAN_POINT ( 'NONE',  ( 6.367873360227556567, 2.886751345948123770, -5.000000000000000000 ) ) ;
#16909=DIRECTION ( 'NONE',  ( 1.000000000000000000, 0.000000000000000000, 0.000000000000000000 ) ) ;
#16941=AXIS2_PLACEMENT_3D ( 'NONE', #2407, #3960, #18781 ) ;
#16943=CARTESIAN_POINT ( 'NONE',  ( 6.518095160331716542, -5.866179305615093931, 2.176274696337492837E-17 ) ) ;
#16946=ORIENTED_EDGE ( 'NONE', *, *, #4975, .T. ) ;
#16987=AXIS2_PLACEMENT_3D ( 'NONE', #5907, #17885, #4449 ) ;
#16988=UNCERTAINTY_MEASURE_WITH_UNIT (LENGTH_MEASURE( 1.000000000000000082E-05 ), #19323, 'distance_accuracy_value', 'NONE');
#17019=FACE_OUTER_BOUND ( 'NONE', #10818, .T. ) ;
#17029=CARTESIAN_POINT ( 'NONE',  ( 6.527192678185835817, -2.941622124011024297, -5.095038975456044561 ) ) ;
#17041=ORIENTED_EDGE ( 'NONE', *, *, #17698, .T. ) ;
#17108=CARTESIAN_POINT ( 'NONE',  ( 6.357987042335720318, 1.995285544161303992, 5.108766985362874102 ) ) ;
#17109=ORIENTED_EDGE ( 'NONE', *, *, #3762, .F. ) ;
#17113=VERTEX_POINT ( 'NONE', #5002 ) ;
#17142=EDGE_LOOP ( 'NONE', ( #11359, #17320, #12527 ) ) ;
#17145=VERTEX_POINT ( 'NONE', #5288 ) ;
#17176=CARTESIAN_POINT ( 'NONE',  ( 6.371506350351446635, 5.409331239960136983, 0.8483282427581467777 ) ) ;
#17193=ORIENTED_EDGE ( 'NONE', *, *, #5799, .F. ) ;
#17219=CARTESIAN_POINT ( 'NONE',  ( 6.367873360227558344, -2.886751345948133984, -5.000000000000000000 ) ) ;
#17230=CARTESIAN_POINT ( 'NONE',  ( 6.495567275915087535, -2.917443832164882345, 5.053160945538040849 ) ) ;
#17231=PLANE ( 'NONE',  #8456 ) ;
#17240=ORIENTED_EDGE ( 'NONE', *, *, #8782, .T. ) ;
#17248=CIRCLE ( 'NONE', #18513, 3.309499999999999886 ) ;
#17283=CARTESIAN_POINT ( 'NONE',  ( 6.242800618755075526, 3.923709308887314950, -3.414402460853798171 ) ) ;
#17298=EDGE_CURVE ( 'NONE', #18807, #3828, #18834, .T. ) ;
#17320=ORIENTED_EDGE ( 'NONE', *, *, #3699, .T. ) ;
#17336=( BOUNDED_SURFACE ( )  B_SPLINE_SURFACE ( 3, 2, ( 
 ( #9446, #3202, #9164 ),
 ( #1918, #10910, #7785 ),
 ( #18393, #7885, #6224 ),
 ( #15142, #13944, #15235 ),
 ( #18297, #7687, #9535 ),
 ( #527, #1719, #624 ) ),
 .UNSPECIFIED., .F., .F., .T. ) 
 B_SPLINE_SURFACE_WITH_KNOTS ( ( 4, 2, 4 ),
 ( 3, 3 ),
 ( 0.02367865728600892020, 0.02663179453327098323, 0.02958493178053304279 ),
 ( 0.000000000000000000, 1.000000000000000000 ),
 .UNSPECIFIED. ) 
 GEOMETRIC_REPRESENTATION_ITEM ( )  RATIONAL_B_SPLINE_SURFACE ( (
 ( 1.000000000000000000, 0.8047781103519402457, 1.000000000000000000),
 ( 1.000000000000000000, 0.8123785825973208752, 1.000000000000000000),
 ( 1.000000000000000000, 0.8190671539297160741, 1.000000000000000000),
 ( 1.000000000000000000, 0.8192352255325974220, 1.000000000000000000),
 ( 1.000000000000000000, 0.8126129676842754890, 1.000000000000000000),
 ( 1.000000000000000000, 0.8047712537969723412, 1.000000000000000000) ) ) 
 REPRESENTATION_ITEM ( '' )  SURFACE ( )  );
#17343=DIRECTION ( 'NONE',  ( -1.000000000000000000, -0.000000000000000000, -0.000000000000000000 ) ) ;
#17363=CARTESIAN_POINT ( 'NONE',  ( 6.092449800118089343, 4.833012432206481357, 1.628976913806340798 ) ) ;
#17375=DIRECTION ( 'NONE',  ( -0.7071067811865530128, 8.659560562354868763E-17, -0.7071067811865421326 ) ) ;
#17378=CARTESIAN_POINT ( 'NONE',  ( 8.500000000000000000, 0.000000000000000000, 0.000000000000000000 ) ) ;
#17402=FACE_OUTER_BOUND ( 'NONE', #18111, .T. ) ;
#17409=CARTESIAN_POINT ( 'NONE',  ( 6.367873360227556567, 2.886751345948123770, -5.000000000000000000 ) ) ;
#17423=CARTESIAN_POINT ( 'NONE',  ( 6.481779955677443361, -2.910222513313286186, 5.040653254389420468 ) ) ;
#17456=DIRECTION ( 'NONE',  ( 0.000000000000000000, 0.000000000000000000, -1.000000000000000000 ) ) ;
#17486=CARTESIAN_POINT ( 'NONE',  ( 6.534838248920900483, -5.903531555104836848, 4.671345613696493211E-16 ) ) ;
#17537=CARTESIAN_POINT ( 'NONE',  ( 0.3106000600989293203, 5.537975084925940372, 0.4079457818577097994 ) ) ;
#17545=EDGE_CURVE ( 'NONE', #1202, #2689, #18170, .T. ) ;
#17547=AXIS2_PLACEMENT_3D ( 'NONE', #3597, #2129, #2239 ) ;
#17580=FACE_OUTER_BOUND ( 'NONE', #11516, .T. ) ;
#17596=CARTESIAN_POINT ( 'NONE',  ( 7.336184427528458230, 0.000000000000000000, -8.105212085995399107 ) ) ;
#17602=FACE_OUTER_BOUND ( 'NONE', #17633, .T. ) ;
#17614=DIRECTION ( 'NONE',  ( -1.000000000000000000, -0.000000000000000000, 0.000000000000000000 ) ) ;
#17633=EDGE_LOOP ( 'NONE', ( #14457, #18530, #18837, #7633, #5550 ) ) ;
#17649=DIRECTION ( 'NONE',  ( 0.000000000000000000, 0.000000000000000000, -1.000000000000000000 ) ) ;
#17668=VERTEX_POINT ( 'NONE', #3812 ) ;
#17698=EDGE_CURVE ( 'NONE', #950, #13007, #7236, .T. ) ;
#17700=ORIENTED_EDGE ( 'NONE', *, *, #4390, .F. ) ;
#17728=ADVANCED_FACE ( 'NONE', ( #10799 ), #9050, .F. ) ;
#17772=CARTESIAN_POINT ( 'NONE',  ( 6.371506350351447523, -5.409331239960139648, -0.8483282427581471108 ) ) ;
#17776=CARTESIAN_POINT ( 'NONE',  ( 8.500000000000000000, 0.000000000000000000, 4.000000000000000000 ) ) ;
#17828=VERTEX_POINT ( 'NONE', #3947 ) ;
#17833=DIRECTION ( 'NONE',  ( 0.000000000000000000, 0.000000000000000000, 1.000000000000000000 ) ) ;
#17843=( NAMED_UNIT ( * ) SI_UNIT ( $, .STERADIAN. ) SOLID_ANGLE_UNIT ( ) );
#17853=CARTESIAN_POINT ( 'NONE',  ( 6.371506350351443082, -3.439339428956426747, 4.260454149911180544 ) ) ;
#17882=AXIS2_PLACEMENT_3D ( 'NONE', #10121, #19376, #11591 ) ;
#17885=DIRECTION ( 'NONE',  ( 1.000000000000000000, 0.000000000000000000, 0.000000000000000000 ) ) ;
#17897=ORIENTED_EDGE ( 'NONE', *, *, #6694, .F. ) ;
#17934=CARTESIAN_POINT ( 'NONE',  ( 6.534838248920897819, 2.951765777552412651, 5.112608298763836601 ) ) ;
#17943=EDGE_CURVE ( 'NONE', #2689, #9187, #4785, .T. ) ;
#17966=CARTESIAN_POINT ( 'NONE',  ( 6.506891779418575439, -5.826362946429633816, -0.09155664655282159947 ) ) ;
#18049=DIRECTION ( 'NONE',  ( 0.000000000000000000, 0.000000000000000000, -1.000000000000000000 ) ) ;
#18061=EDGE_CURVE ( 'NONE', #950, #2819, #9453, .T. ) ;
#18087=CIRCLE ( 'NONE', #5857, 4.000000000000000000 ) ;
#18110=DIRECTION ( 'NONE',  ( 0.000000000000000000, 0.000000000000000000, 1.000000000000000000 ) ) ;
#18111=EDGE_LOOP ( 'NONE', ( #1660, #2800 ) ) ;
#18132=EDGE_LOOP ( 'NONE', ( #11596, #17240, #7432 ) ) ;
#18136=EDGE_LOOP ( 'NONE', ( #10035, #1558, #12886, #4509, #3233, #11214, #16946 ) ) ;
#18170=B_SPLINE_CURVE_WITH_KNOTS ( 'NONE', 3,
 ( #10567, #10669, #17853, #6170, #3238, #9198, #4514, #9005 ),
 .UNSPECIFIED., .F., .F.,
 ( 4, 2, 2, 4 ),
 ( 0.000000000000000000, 0.001493104274552342322, 0.002986208549104684210, 0.005972417098209366684 ),
 .UNSPECIFIED. ) ;
#18171=EDGE_CURVE ( 'NONE', #17145, #950, #18371, .T. ) ;
#18181=FACE_OUTER_BOUND ( 'NONE', #10865, .T. ) ;
#18183=ADVANCED_FACE ( 'NONE', ( #17580 ), #18710, .F. ) ;
#18189=AXIS2_PLACEMENT_3D ( 'NONE', #1689, #18264, #13635 ) ;
#18216=ORIENTED_EDGE ( 'NONE', *, *, #2156, .F. ) ;
#18218=AXIS2_PLACEMENT_3D ( 'NONE', #15376, #1957, #12426 ) ;
#18219=EDGE_CURVE ( 'NONE', #18786, #4901, #6563, .T. ) ;
#18233=CARTESIAN_POINT ( 'NONE',  ( 6.403457969954083673, -5.776886471390910494, 4.740078563816561288E-16 ) ) ;
#18237=DIRECTION ( 'NONE',  ( 0.000000000000000000, 0.000000000000000000, 1.000000000000000000 ) ) ;
#18264=DIRECTION ( 'NONE',  ( 1.000000000000000000, 0.000000000000000000, 0.000000000000000000 ) ) ;
#18270=EDGE_CURVE ( 'NONE', #18339, #17828, #11535, .T. ) ;
#18295=AXIS2_PLACEMENT_3D ( 'NONE', #9238, #1624, #16427 ) ;
#18297=CARTESIAN_POINT ( 'NONE',  ( 6.207671477328757348, -5.338259717474211463, -0.7538629453363940858 ) ) ;
#18339=VERTEX_POINT ( 'NONE', #12993 ) ;
#18368=CARTESIAN_POINT ( 'NONE',  ( 6.244004651191001010, 4.663678638742294602, 2.132808149174402867 ) ) ;
#18371=B_SPLINE_CURVE_WITH_KNOTS ( 'NONE', 3,
 ( #8922, #14904, #1477, #7455 ),
 .UNSPECIFIED., .F., .F.,
 ( 4, 4 ),
 ( 2.380735200831979558E-07, 0.002921158011986727237 ),
 .UNSPECIFIED. ) ;
#18393=CARTESIAN_POINT ( 'NONE',  ( 6.095473853218072335, -3.806361898857768544, -3.407187799184005161 ) ) ;
#18394=ORIENTED_EDGE ( 'NONE', *, *, #19173, .T. ) ;
#18408=PLANE ( 'NONE',  #13513 ) ;
#18416=ADVANCED_FACE ( 'NONE', ( #9846 ), #17231, .F. ) ;
#18421=DIRECTION ( 'NONE',  ( -1.000000000000000000, -0.000000000000000000, -0.000000000000000000 ) ) ;
#18473=CARTESIAN_POINT ( 'NONE',  ( 6.436591462021363341, 2.894509378375959674, -5.013437306331780086 ) ) ;
#18504=CARTESIAN_POINT ( 'NONE',  ( 6.534224484704326485, -2.950930484791631780, -5.111161529262894909 ) ) ;
#18508=CARTESIAN_POINT ( 'NONE',  ( 6.367873360227556567, 2.886751345948125991, 4.999999999999999112 ) ) ;
#18510=CARTESIAN_POINT ( 'NONE',  ( 7.900000000000002132, 0.000000000000000000, 7.900000000000002132 ) ) ;
#18513=AXIS2_PLACEMENT_3D ( 'NONE', #4482, #10440, #16348 ) ;
#18529=VECTOR ( 'NONE', #11238, 1000.000000000000114 ) ;
#18530=ORIENTED_EDGE ( 'NONE', *, *, #12394, .T. ) ;
#18566=CARTESIAN_POINT ( 'NONE',  ( 8.500000000000000000, -2.886751345948119774, 4.999999999999999112 ) ) ;
#18582=CARTESIAN_POINT ( 'NONE',  ( 0.4465819873852006072, 2.886751345948123770, -5.000000000000000000 ) ) ;
#18603=CARTESIAN_POINT ( 'NONE',  ( 6.534533895392296010, -2.951347675328743314, -5.111884124469654900 ) ) ;
#18613=CARTESIAN_POINT ( 'NONE',  ( 6.367873360227555679, -2.886751345948119774, 4.999999999999999112 ) ) ;
#18614=CARTESIAN_POINT ( 'NONE',  ( 6.242800618755128816, -3.923709308886856206, 3.414402460854895072 ) ) ;
#18681=CARTESIAN_POINT ( 'NONE',  ( 6.323290364500451233, 2.010128762267162639, 4.999999999999998224 ) ) ;
#18689=CIRCLE ( 'NONE', #13351, 4.999999999999999112 ) ;
#18707=CARTESIAN_POINT ( 'NONE',  ( 53.50000000000000000, 0.000000000000000000, 0.000000000000000000 ) ) ;
#18710=( BOUNDED_SURFACE ( )  B_SPLINE_SURFACE ( 3, 2, ( 
 ( #5154, #17966, #5062 ),
 ( #15000, #3153, #12058 ),
 ( #9119, #4525, #656 ),
 ( #7742, #12, #18614 ),
 ( #10483, #15654, #16486 ),
 ( #6000, #13537, #4618 ) ),
 .UNSPECIFIED., .F., .F., .F. ) 
 B_SPLINE_SURFACE_WITH_KNOTS ( ( 4, 2, 4 ),
 ( 3, 3 ),
 ( 0.02367865728600888897, 0.02663179453327094853, 0.02958493178053300809 ),
 ( 0.000000000000000000, 1.000000000000000000 ),
 .UNSPECIFIED. ) 
 GEOMETRIC_REPRESENTATION_ITEM ( )  RATIONAL_B_SPLINE_SURFACE ( (
 ( 1.000000000000000000, 0.8047781103519399126, 1.000000000000000000),
 ( 1.000000000000000000, 0.8123785825980039954, 1.000000000000000000),
 ( 1.000000000000000000, 0.8190671539288042480, 1.000000000000000000),
 ( 1.000000000000000000, 0.8192352255335092481, 1.000000000000000000),
 ( 1.000000000000000000, 0.8126129676835893711, 1.000000000000000000),
 ( 1.000000000000000000, 0.8047712537969730073, 1.000000000000000000) ) ) 
 REPRESENTATION_ITEM ( '' )  SURFACE ( )  );
#18736=ADVANCED_FACE ( 'NONE', ( #17019 ), #17336, .F. ) ;
#18754=CARTESIAN_POINT ( 'NONE',  ( 6.390820841722129941, 5.837016270311235822, 0.1100087447852453187 ) ) ;
#18759=DIRECTION ( 'NONE',  ( -0.000000000000000000, 0.8660254037844387076, 0.5000000000000001110 ) ) ;
#18781=DIRECTION ( 'NONE',  ( -0.000000000000000000, 0.000000000000000000, -1.000000000000000000 ) ) ;
#18786=VERTEX_POINT ( 'NONE', #5419 ) ;
#18805=CARTESIAN_POINT ( 'NONE',  ( 6.534838248920896930, -2.951765777552406878, 5.112608298763836601 ) ) ;
#18807=VERTEX_POINT ( 'NONE', #8358 ) ;
#18819=ORIENTED_EDGE ( 'NONE', *, *, #3817, .F. ) ;
#18834=CIRCLE ( 'NONE', #16005, 4.000000000000000000 ) ;
#18837=ORIENTED_EDGE ( 'NONE', *, *, #6608, .T. ) ;
#18845=CARTESIAN_POINT ( 'NONE',  ( 6.212068001622437663, 3.310128279683251851, 4.266689640018040741 ) ) ;
#18847=DIRECTION ( 'NONE',  ( 0.000000000000000000, 0.000000000000000000, -1.000000000000000000 ) ) ;
#18859=CARTESIAN_POINT ( 'NONE',  ( 6.207530437345012864, 4.849805425595251407, -1.599890596046337210 ) ) ;
#18860=B_SPLINE_CURVE_WITH_KNOTS ( 'NONE', 3,
 ( #13405, #9270, #3223, #15168, #3504 ),
 .UNSPECIFIED., .F., .F.,
 ( 4, 1, 4 ),
 ( 0.000000000000000000, 0.002886751345948128985, 0.005773502691896257970 ),
 .UNSPECIFIED. ) ;
#18883=ADVANCED_FACE ( 'NONE', ( #4059 ), #1177, .F. ) ;
#18886=ORIENTED_EDGE ( 'NONE', *, *, #10943, .T. ) ;
#18898=DIRECTION ( 'NONE',  ( 0.000000000000000000, -0.8660254037844380415, 0.5000000000000011102 ) ) ;
#18905=ADVANCED_FACE ( 'NONE', ( #12779, #17402 ), #15824, .T. ) ;
#18906=CARTESIAN_POINT ( 'NONE',  ( 6.518095160331717430, -2.933089652807539416, 5.080260301817235202 ) ) ;
#18922=CARTESIAN_POINT ( 'NONE',  ( 8.500000000000000000, -2.886751345948133984, -5.000000000000000000 ) ) ;
#18938=CARTESIAN_POINT ( 'NONE',  ( 6.385552186430389021, 5.773502691896261751, 0.000000000000000000 ) ) ;
#18941=ADVANCED_FACE ( 'NONE', ( #7573 ), #8778, .T. ) ;
#18948=EDGE_CURVE ( 'NONE', #7769, #13093, #11600, .T. ) ;
#19017=CARTESIAN_POINT ( 'NONE',  ( 0.1983443223721582938, 5.300482436767278038, 0.8192951148925896598 ) ) ;
#19033=CARTESIAN_POINT ( 'NONE',  ( 0.000000000000000000, 4.330127018922190985, 2.500000000000005329 ) ) ;
#19039=ORIENTED_EDGE ( 'NONE', *, *, #651, .T. ) ;
#19077=CARTESIAN_POINT ( 'NONE',  ( 6.207682235857189035, 2.016324304256315258, 4.999999999999999112 ) ) ;
#19089=CARTESIAN_POINT ( 'NONE',  ( 0.1973348417602843741, -1.936114729415326696, -5.000000000000000000 ) ) ;
#19139=ADVANCED_FACE ( 'NONE', ( #17602 ), #8852, .F. ) ;
#19150=CIRCLE ( 'NONE', #12845, 4.999999999999999112 ) ;
#19169=CARTESIAN_POINT ( 'NONE',  ( 6.244004651191001010, -4.663678638742299931, -2.132808149174403312 ) ) ;
#19173=EDGE_CURVE ( 'NONE', #4901, #17113, #10703, .T. ) ;
#19185=STYLED_ITEM('',(#19475),#2357);
#19187=DIRECTION ( 'NONE',  ( -0.000000000000000000, 0.000000000000000000, 1.000000000000000000 ) ) ;
#19192=ORIENTED_EDGE ( 'NONE', *, *, #18948, .T. ) ;
#19241=DIRECTION ( 'NONE',  ( 0.000000000000000000, -1.224646799147353700E-16, 1.000000000000000000 ) ) ;
#19258=CARTESIAN_POINT ( 'NONE',  ( 6.534838248920899595, -2.951765777552420644, -5.112608298763837489 ) ) ;
#19263=CARTESIAN_POINT ( 'NONE',  ( 6.445127866599367650, -5.657054305385780246, -0.4229901806197432501 ) ) ;
#19277=ORIENTED_EDGE ( 'NONE', *, *, #5799, .T. ) ;
#19278=B_SPLINE_CURVE_WITH_KNOTS ( 'NONE', 3,
 ( #6366, #9400, #1967, #486, #3529, #15478 ),
 .UNSPECIFIED., .F., .F.,
 ( 4, 2, 4 ),
 ( 0.005339748439308726613, 0.006800846765732536554, 0.008261945092156346496 ),
 .UNSPECIFIED. ) ;
#19281=ORIENTED_EDGE ( 'NONE', *, *, #3350, .T. ) ;
#19323=( LENGTH_UNIT ( ) NAMED_UNIT ( * ) SI_UNIT ( .MILLI., .METRE. ) );
#19330=FILL_AREA_STYLE_COLOUR ( '', #15607 ) ;
#19334=VERTEX_POINT ( 'NONE', #1990 ) ;
#19339=UNCERTAINTY_MEASURE_WITH_UNIT (LENGTH_MEASURE( 1.000000000000000082E-05 ), #8900, 'distance_accuracy_value', 'NONE');
#19376=DIRECTION ( 'NONE',  ( -1.000000000000000000, -0.000000000000000000, -0.000000000000000000 ) ) ;
#19387=EDGE_LOOP ( 'NONE', ( #899, #15727 ) ) ;
#19412=DIRECTION ( 'NONE',  ( 0.000000000000000000, 0.000000000000000000, -1.000000000000000000 ) ) ;
#19469=COLOUR_RGB('Black',0.12,0.14,0.17);
#19470=FILL_AREA_STYLE_COLOUR('',#19469);
#19471=FILL_AREA_STYLE('',(#19470));
#19472=SURFACE_STYLE_FILL_AREA(#19471);
#19473=SURFACE_SIDE_STYLE('',(#19472));
#19474=SURFACE_STYLE_USAGE(.BOTH.,#19473);
#19475=PRESENTATION_STYLE_ASSIGNMENT((#19474));
ENDSEC;
END-ISO-10303-21;
